ISO-10303-21;
HEADER;
FILE_DESCRIPTION (('STEP AP203'),
    '1' );
FILE_NAME ('bench vise3-.step',
    '2026-10-07T23:37:23',
    ( '' ),
    ( '' ),
    'SwSTEP 2.0',
    'SolidWorks 2024',
    '' );
FILE_SCHEMA (( 'AUTOMOTIVE_DESIGN' ));
ENDSEC;

DATA;
#17=ORIENTED_EDGE ( 'NONE', *, *, #5224, .F. ) ;
#20=CARTESIAN_POINT ( 'NONE',  ( -1.187499999999999778, 4.475358323637860458, 6.462174474937253166 ) ) ;
#22=ORIENTED_EDGE ( 'NONE', *, *, #441, .F. ) ;
#29=CARTESIAN_POINT ( 'NONE',  ( -2.750000000000000444, 8.601289606299213020, 5.246732086614174229 ) ) ;
#56=CARTESIAN_POINT ( 'NONE',  ( 2.750000000000000444, 8.601278779527561369, 5.246694173228347857 ) ) ;
#68=CARTESIAN_POINT ( 'NONE',  ( -1.187500000000000000, 4.528589268181947070, 6.350981843454763798 ) ) ;
#76=PLANE ( 'NONE',  #326 ) ;
#81=ORIENTED_EDGE ( 'NONE', *, *, #8030, .T. ) ;
#102=ADVANCED_FACE ( 'NONE', ( #760 ), #2649, .T. ) ;
#108=CARTESIAN_POINT ( 'NONE',  ( 2.750000000000000444, 8.574153543307087233, 4.323749999999999538 ) ) ;
#117=ORIENTED_EDGE ( 'NONE', *, *, #7488, .F. ) ;
#141=ORIENTED_EDGE ( 'NONE', *, *, #2782, .T. ) ;
#165=CIRCLE ( 'NONE', #6062, 1.074999999999999289 ) ;
#199=AXIS2_PLACEMENT_3D ( 'NONE', #677, #1458, #2606 ) ;
#201=CARTESIAN_POINT ( 'NONE',  ( -2.750000000000000444, 7.541160346212514298, 3.932968645167688404 ) ) ;
#204=ORIENTED_EDGE ( 'NONE', *, *, #4799, .T. ) ;
#230=DIRECTION ( 'NONE',  ( -0.000000000000000000, -0.000000000000000000, 1.000000000000000000 ) ) ;
#239=EDGE_CURVE ( 'NONE', #5017, #7058, #2139, .T. ) ;
#246=CARTESIAN_POINT ( 'NONE',  ( 1.187500000000000444, 4.987711023622046547, 4.083473622047245399 ) ) ;
#252=EDGE_CURVE ( 'NONE', #2515, #533, #7031, .T. ) ;
#255=DIRECTION ( 'NONE',  ( -0.000000000000000000, -0.000000000000000000, 1.000000000000000000 ) ) ;
#291=( NAMED_UNIT ( * ) PLANE_ANGLE_UNIT ( ) SI_UNIT ( $, .RADIAN. ) );
#307=CARTESIAN_POINT ( 'NONE',  ( 1.074999999999999289, 3.950000000000000178, -4.043750000000001066 ) ) ;
#316=CARTESIAN_POINT ( 'NONE',  ( 0.000000000000000000, 5.541000000000003034, 3.956250000000000266 ) ) ;
#318=CARTESIAN_POINT ( 'NONE',  ( -1.388463899750249738E-31, 3.950000000000000178, -4.043750000000001066 ) ) ;
#320=CARTESIAN_POINT ( 'NONE',  ( -2.577468385826771957, 5.238734212598424200, 3.956250000000000266 ) ) ;
#326=AXIS2_PLACEMENT_3D ( 'NONE', #29, #2593, #1974 ) ;
#351=CARTESIAN_POINT ( 'NONE',  ( -2.750000000000000444, 7.964000000000000412, 5.246732086614174229 ) ) ;
#383=CARTESIAN_POINT ( 'NONE',  ( 2.375000000000000888, 2.762500000000000178, 6.956249999999999822 ) ) ;
#401=DIRECTION ( 'NONE',  ( -1.000000000000000000, -0.000000000000000000, -0.000000000000000000 ) ) ;
#441=EDGE_CURVE ( 'NONE', #5098, #1162, #5449, .T. ) ;
#442=VERTEX_POINT ( 'NONE', #3979 ) ;
#467=FACE_OUTER_BOUND ( 'NONE', #758, .T. ) ;
#484=DIRECTION ( 'NONE',  ( 0.000000000000000000, 0.000000000000000000, -1.000000000000000000 ) ) ;
#491=CARTESIAN_POINT ( 'NONE',  ( -1.187500000000000444, 7.964000000000000412, 5.236250000000000071 ) ) ;
#492=VECTOR ( 'NONE', #6658, 39.37007874015748143 ) ;
#494=FACE_OUTER_BOUND ( 'NONE', #8010, .T. ) ;
#502=ORIENTED_EDGE ( 'NONE', *, *, #7720, .T. ) ;
#504=CARTESIAN_POINT ( 'NONE',  ( 2.749999999999999556, 7.339000000000003077, 4.175863149606300340 ) ) ;
#510=DIRECTION ( 'NONE',  ( 5.213780441972162403E-17, -8.342048707155459845E-16, -1.000000000000000000 ) ) ;
#533=VERTEX_POINT ( 'NONE', #5878 ) ;
#565=CARTESIAN_POINT ( 'NONE',  ( 0.000000000000000000, 5.153197523761609666, 6.890983900766838310 ) ) ;
#587=AXIS2_PLACEMENT_3D ( 'NONE', #2371, #4861, #1141 ) ;
#603=CARTESIAN_POINT ( 'NONE',  ( 0.000000000000000000, 5.024999999999999467, 3.742515787401575533 ) ) ;
#621=AXIS2_PLACEMENT_3D ( 'NONE', #7518, #3053, #3755 ) ;
#630=( BOUNDED_CURVE ( )  B_SPLINE_CURVE ( 3, ( #643, #5097, #3106, #4364 ),
 .UNSPECIFIED., .F., .F. ) 
 B_SPLINE_CURVE_WITH_KNOTS ( ( 4, 4 ),
 ( 0.000000000000000000, 0.09428240746600520528 ),
 .UNSPECIFIED. ) 
 CURVE ( )  GEOMETRIC_REPRESENTATION_ITEM ( )  RATIONAL_B_SPLINE_CURVE ( ( 1.000000000000000000, 0.3333333333333330373, 0.3333333333333330373, 1.000000000000000000 ) ) 
 REPRESENTATION_ITEM ( '' )  );
#643=CARTESIAN_POINT ( 'NONE',  ( 0.000000000000000000, 2.762500000000000178, 6.956250000000000711 ) ) ;
#647=FACE_OUTER_BOUND ( 'NONE', #2462, .T. ) ;
#654=CARTESIAN_POINT ( 'NONE',  ( -2.750000000000000444, 7.521783346469146814, 3.956249999992520916 ) ) ;
#677=CARTESIAN_POINT ( 'NONE',  ( -1.388463899750249738E-31, 3.950000000000000178, -4.043750000000001066 ) ) ;
#678=CARTESIAN_POINT ( 'NONE',  ( 1.187500000000000222, 8.351123808915705382, 5.236250000000000959 ) ) ;
#694=CARTESIAN_POINT ( 'NONE',  ( 0.000000000000000000, 2.359000000000000874, 3.956250000000000266 ) ) ;
#717=CIRCLE ( 'NONE', #5284, 1.074999999999999289 ) ;
#723=CARTESIAN_POINT ( 'NONE',  ( 0.000000000000000000, 2.359000000000000874, 3.956250000000000266 ) ) ;
#724=LINE ( 'NONE', #4939, #3752 ) ;
#758=EDGE_LOOP ( 'NONE', ( #3244, #6684, #4289, #6147 ) ) ;
#760=FACE_OUTER_BOUND ( 'NONE', #4077, .T. ) ;
#775=CARTESIAN_POINT ( 'NONE',  ( -2.750000000000000444, 8.589000000000000412, 5.236250000000000071 ) ) ;
#779=CARTESIAN_POINT ( 'NONE',  ( -1.187500000000001110, 4.823637706830838923, 5.420136398917323461 ) ) ;
#787=ORIENTED_EDGE ( 'NONE', *, *, #1133, .T. ) ;
#789=VERTEX_POINT ( 'NONE', #2233 ) ;
#802=CARTESIAN_POINT ( 'NONE',  ( 2.750000000000000444, 7.964000000000001300, 3.956250000085291152 ) ) ;
#805=VERTEX_POINT ( 'NONE', #7201 ) ;
#814=CARTESIAN_POINT ( 'NONE',  ( 2.750000000000000444, 7.521783346456695440, 3.956250000000000266 ) ) ;
#851=EDGE_LOOP ( 'NONE', ( #2608, #7946, #1251, #2754, #2509 ) ) ;
#857=LINE ( 'NONE', #246, #1893 ) ;
#864=LENGTH_MEASURE_WITH_UNIT ( LENGTH_MEASURE( 0.02539999999999999897 ), #4629 );
#875=CARTESIAN_POINT ( 'NONE',  ( 0.000000000000000000, 2.523992677165354692, 5.972081456692915680 ) ) ;
#909=CARTESIAN_POINT ( 'NONE',  ( -1.074999999999999289, 3.950000000000000178, 3.440250000000000696 ) ) ;
#921=EDGE_CURVE ( 'NONE', #7981, #7410, #5112, .T. ) ;
#937=CARTESIAN_POINT ( 'NONE',  ( -2.150000000000000799, 2.875000000000000888, 3.440250000000000696 ) ) ;
#945=LINE ( 'NONE', #7829, #4536 ) ;
#956=ADVANCED_FACE ( 'NONE', ( #2283 ), #2211, .T. ) ;
#975=CYLINDRICAL_SURFACE ( 'NONE', #5703, 1.074999999999999289 ) ;
#980=AXIS2_PLACEMENT_3D ( 'NONE', #7572, #3273, #2582 ) ;
#981=EDGE_LOOP ( 'NONE', ( #1160, #4241, #22, #3595, #17 ) ) ;
#1023=CARTESIAN_POINT ( 'NONE',  ( 0.000000000000000000, 5.238734212598425088, 3.956250000000001155 ) ) ;
#1048=ORIENTED_EDGE ( 'NONE', *, *, #4471, .T. ) ;
#1081=CARTESIAN_POINT ( 'NONE',  ( -1.187500000000000222, 5.969165905511811587, 4.238473622047244760 ) ) ;
#1082=EDGE_CURVE ( 'NONE', #5017, #5232, #7856, .T. ) ;
#1117=VERTEX_POINT ( 'NONE', #2461 ) ;
#1123=DIRECTION ( 'NONE',  ( 1.000000000000000000, 0.000000000000000000, 0.000000000000000000 ) ) ;
#1132=CARTESIAN_POINT ( 'NONE',  ( 1.187499999999999778, 4.331466137858002163, 6.700178998068949454 ) ) ;
#1133=EDGE_CURVE ( 'NONE', #3502, #5894, #724, .T. ) ;
#1141=DIRECTION ( 'NONE',  ( 0.000000000000000000, 0.000000000000000000, 1.000000000000000000 ) ) ;
#1159=CARTESIAN_POINT ( 'NONE',  ( 0.000000000000000000, 2.389005866141733492, 4.968462007874015818 ) ) ;
#1160=ORIENTED_EDGE ( 'NONE', *, *, #5479, .F. ) ;
#1162=VERTEX_POINT ( 'NONE', #4160 ) ;
#1167=DIRECTION ( 'NONE',  ( -0.000000000000000000, -0.000000000000000000, 1.000000000000000000 ) ) ;
#1186=VERTEX_POINT ( 'NONE', #6372 ) ;
#1198=ORIENTED_EDGE ( 'NONE', *, *, #6772, .F. ) ;
#1203=CARTESIAN_POINT ( 'NONE',  ( 1.187500000000000444, 4.598373714026829262, 6.183596452058795379 ) ) ;
#1209=CARTESIAN_POINT ( 'NONE',  ( 0.8527717968728635300, 5.380045629463952928, 4.083473622047246288 ) ) ;
#1225=CARTESIAN_POINT ( 'NONE',  ( 0.000000000000000000, 5.160877715062512472, 6.858307716807694909 ) ) ;
#1238=ORIENTED_EDGE ( 'NONE', *, *, #1082, .F. ) ;
#1239=CIRCLE ( 'NONE', #2027, 1.074999999999999289 ) ;
#1250=CARTESIAN_POINT ( 'NONE',  ( 1.187500000000000666, 4.964596198445718755, 4.572665754078526490 ) ) ;
#1251=ORIENTED_EDGE ( 'NONE', *, *, #5093, .F. ) ;
#1258=CARTESIAN_POINT ( 'NONE',  ( 0.000000000000000000, 2.875000000000000888, 3.440250000000001140 ) ) ;
#1265=CARTESIAN_POINT ( 'NONE',  ( -1.388463899750249738E-31, 3.950000000000000178, -4.043750000000001066 ) ) ;
#1278=CARTESIAN_POINT ( 'NONE',  ( -1.187500000000000444, 4.233290553842588899, 6.816515182600094924 ) ) ;
#1287=ORIENTED_EDGE ( 'NONE', *, *, #1336, .F. ) ;
#1291=CARTESIAN_POINT ( 'NONE',  ( 1.187500000000000444, 4.680108205028392199, 5.951860652718446332 ) ) ;
#1298=CARTESIAN_POINT ( 'NONE',  ( 0.000000000000000000, 5.541000000000003034, 3.956250000000000266 ) ) ;
#1303=( BOUNDED_SURFACE ( )  B_SPLINE_SURFACE ( 3, 3, ( 
 ( #4178, #383, #3577, #4757 ),
 ( #2353, #4215, #7417, #6735 ),
 ( #1159, #2227, #5521, #4302 ),
 ( #694, #4383, #3769, #5572 ) ),
 .UNSPECIFIED., .F., .F., .T. ) 
 B_SPLINE_SURFACE_WITH_KNOTS ( ( 4, 4 ),
 ( 4, 4 ),
 ( 0.000000000000000000, 1.000000000000000000 ),
 ( 0.000000000000000000, 1.000000000000000000 ),
 .UNSPECIFIED. ) 
 GEOMETRIC_REPRESENTATION_ITEM ( )  RATIONAL_B_SPLINE_SURFACE ( (
 ( 1.000000000000000000, 0.3333333333333330373, 0.3333333333333330373, 1.000000000000000000),
 ( 0.9963935896217739341, 0.3321311965405909783, 0.3321311965405909783, 0.9963935896217739341),
 ( 0.9963935896217739341, 0.3321311965405909783, 0.3321311965405909783, 0.9963935896217739341),
 ( 1.000000000000000000, 0.3333333333333330373, 0.3333333333333330373, 1.000000000000000000) ) ) 
 REPRESENTATION_ITEM ( '' )  SURFACE ( )  );
#1309=CARTESIAN_POINT ( 'NONE',  ( -2.750000000000000444, 8.574153543168254288, 4.323749999249341336 ) ) ;
#1336=EDGE_CURVE ( 'NONE', #805, #789, #5448, .T. ) ;
#1341=ADVANCED_BREP_SHAPE_REPRESENTATION ( '', ( #7864, #7272 ), #2017 ) ;
#1346=CARTESIAN_POINT ( 'NONE',  ( -2.750000000000000444, 7.339000000000003077, 4.175863149606300340 ) ) ;
#1349=CARTESIAN_POINT ( 'NONE',  ( 2.750000000000000444, 7.964000000000000412, 5.236250000000000071 ) ) ;
#1366=VERTEX_POINT ( 'NONE', #4874 ) ;
#1374=VECTOR ( 'NONE', #5430, 39.37007874015748143 ) ;
#1391=CARTESIAN_POINT ( 'NONE',  ( 0.000000000000000000, 7.521783346469146814, 3.956249999985041566 ) ) ;
#1392=CARTESIAN_POINT ( 'NONE',  ( 0.000000000000000000, 5.536672282146935409, 4.083473622047245399 ) ) ;
#1396=CARTESIAN_POINT ( 'NONE',  ( -2.750000000000000444, 7.339000000000003077, 5.236250000000000071 ) ) ;
#1399=CARTESIAN_POINT ( 'NONE',  ( 2.750000000000000444, 7.541160346212514298, 3.932968645167688404 ) ) ;
#1418=ORIENTED_EDGE ( 'NONE', *, *, #8044, .T. ) ;
#1419=PRODUCT_DEFINITION ( 'UNKNOWN', '', #6576, #7966 ) ;
#1422=CARTESIAN_POINT ( 'NONE',  ( 2.150000000000000799, 2.875000000000000888, 3.440250000000000696 ) ) ;
#1434=VERTEX_POINT ( 'NONE', #7578 ) ;
#1440=CARTESIAN_POINT ( 'NONE',  ( -2.750000000000000444, 7.964000000000000412, 5.236250000000000071 ) ) ;
#1458=DIRECTION ( 'NONE',  ( 0.000000000000000000, 0.000000000000000000, -1.000000000000000000 ) ) ;
#1473=CARTESIAN_POINT ( 'NONE',  ( -1.187500000000000000, 8.523567361455139491, 4.820336051656679999 ) ) ;
#1474=ORIENTED_EDGE ( 'NONE', *, *, #3382, .T. ) ;
#1475=CARTESIAN_POINT ( 'NONE',  ( -1.187500000000000000, 4.964569481811528462, 4.572968553284305848 ) ) ;
#1482=SHAPE_REPRESENTATION_RELATIONSHIP ( 'NONE' , 'NONE' ,  #4229, #1341 ) ;
#1487=ORIENTED_EDGE ( 'NONE', *, *, #2898, .F. ) ;
#1499=CARTESIAN_POINT ( 'NONE',  ( 2.750000000000000444, 8.601278779527561369, 3.956250000127937483 ) ) ;
#1514=ORIENTED_EDGE ( 'NONE', *, *, #7488, .T. ) ;
#1595=ADVANCED_FACE ( 'NONE', ( #5742 ), #1303, .T. ) ;
#1613=DIRECTION ( 'NONE',  ( -1.000000000000000000, 0.000000000000000000, 0.000000000000000000 ) ) ;
#1620=DIRECTION ( 'NONE',  ( 1.000000000000000000, 0.000000000000000000, -1.986798540846736797E-16 ) ) ;
#1647=CARTESIAN_POINT ( 'NONE',  ( 1.074999999999999289, 3.950000000000000178, -4.043750000000001066 ) ) ;
#1657=ORIENTED_EDGE ( 'NONE', *, *, #4038, .T. ) ;
#1673=CARTESIAN_POINT ( 'NONE',  ( 0.000000000000000000, 2.762500000000000178, 6.956250000000000711 ) ) ;
#1685=CARTESIAN_POINT ( 'NONE',  ( 2.750000000000000444, 7.964000000000001300, 4.323750000000001315 ) ) ;
#1689=CARTESIAN_POINT ( 'NONE',  ( 2.750000000000000444, 8.574153540863029832, 4.323750000000001315 ) ) ;
#1697=DIRECTION ( 'NONE',  ( 1.000000000000000000, 0.000000000000000000, -1.986798540846736797E-16 ) ) ;
#1715=CARTESIAN_POINT ( 'NONE',  ( -2.750000000000000444, 7.521783346456694552, 3.956250000000000266 ) ) ;
#1723=CARTESIAN_POINT ( 'NONE',  ( 1.187500001445445985, 5.969165905511811587, 6.858307716535433585 ) ) ;
#1730=( BOUNDED_SURFACE ( )  B_SPLINE_SURFACE ( 2, 1, ( 
 ( #2708, #108 ),
 ( #4420, #7011 ),
 ( #5734, #6926 ),
 ( #3839, #4545 ),
 ( #1440, #1349 ),
 ( #3915, #6436 ),
 ( #7615, #7091 ),
 ( #2623, #5644 ),
 ( #3951, #814 ),
 ( #3313, #5816 ),
 ( #201, #1399 ) ),
 .UNSPECIFIED., .F., .F., .F. ) 
 B_SPLINE_SURFACE_WITH_KNOTS ( ( 3, 2, 2, 2, 2, 3 ),
 ( 2, 2 ),
 ( 1.337827206813319902, 1.570796326794899889, 3.141592653589790007, 4.712388980384690562, 5.497197239955629477, 5.538790940287052322 ),
 ( 0.000000000000000000, 1.000000000000000000 ),
 .UNSPECIFIED. ) 
 GEOMETRIC_REPRESENTATION_ITEM ( )  RATIONAL_B_SPLINE_SURFACE ( (
 ( 0.9260057553135141450, 0.9260057553135141450),
 ( 0.9565602018087399072, 0.9565602018087399072),
 ( 1.000000000000000000, 1.000000000000000000),
 ( 0.7071067811865479058, 0.7071067811865479058),
 ( 1.000000000000000000, 1.000000000000000000),
 ( 0.7071067811865479058, 0.7071067811865479058),
 ( 1.000000000000000000, 1.000000000000000000),
 ( 0.8536633850130399548, 0.8536633850130399548),
 ( 0.8535534732088591037, 0.8535534732088591037),
 ( 0.8535534732088591037, 0.8535534732088591037),
 ( 0.8535534732088591037, 0.8535534732088591037) ) ) 
 REPRESENTATION_ITEM ( '' )  SURFACE ( )  );
#1739=CARTESIAN_POINT ( 'NONE',  ( -1.187500000000000222, 5.969165905511811587, 6.858307716535433585 ) ) ;
#1750=CARTESIAN_POINT ( 'NONE',  ( 1.187500000000000000, 5.002317768095269734, 4.083473622031662309 ) ) ;
#1786=DIRECTION ( 'NONE',  ( 1.000000000000000000, -0.000000000000000000, 0.000000000000000000 ) ) ;
#1810=EDGE_CURVE ( 'NONE', #5001, #1117, #4252, .T. ) ;
#1813=EDGE_LOOP ( 'NONE', ( #4739, #6012, #6904, #1474, #6779 ) ) ;
#1824=CARTESIAN_POINT ( 'NONE',  ( 1.187499999999999778, 4.894190003925942278, 5.057715191908433106 ) ) ;
#1838=DIRECTION ( 'NONE',  ( 1.000000000000000000, 0.000000000000000000, 0.000000000000000000 ) ) ;
#1864=FACE_OUTER_BOUND ( 'NONE', #5147, .T. ) ;
#1867=ORIENTED_EDGE ( 'NONE', *, *, #6601, .F. ) ;
#1869=DIRECTION ( 'NONE',  ( -0.000000000000000000, -0.000000000000000000, 1.000000000000000000 ) ) ;
#1883=CARTESIAN_POINT ( 'NONE',  ( -0.5199956508225699325, 5.160877715126506615, 6.858307716535431808 ) ) ;
#1890=DIRECTION ( 'NONE',  ( 0.000000000000000000, 0.000000000000000000, -1.000000000000000000 ) ) ;
#1893=VECTOR ( 'NONE', #5936, 39.37007874015748143 ) ;
#1900=CARTESIAN_POINT ( 'NONE',  ( 1.187500000000000444, 4.399518635675126355, 6.597653535770707123 ) ) ;
#1926=CARTESIAN_POINT ( 'NONE',  ( -1.187499999443275334, 5.002317768720649482, 4.083473622047245399 ) ) ;
#1931=EDGE_CURVE ( 'NONE', #2515, #6380, #4914, .T. ) ;
#1944=CARTESIAN_POINT ( 'NONE',  ( 1.187499999999999334, 4.294112494781764156, 6.748660968904401258 ) ) ;
#1965=VERTEX_POINT ( 'NONE', #3270 ) ;
#1966=CARTESIAN_POINT ( 'NONE',  ( -1.187500000000000666, 4.894061234189001297, 5.058487564149448446 ) ) ;
#1974=DIRECTION ( 'NONE',  ( 0.000000000000000000, 0.000000000000000000, -1.000000000000000000 ) ) ;
#1990=DIRECTION ( 'NONE',  ( 0.000000000000000000, 0.000000000000000000, -1.000000000000000000 ) ) ;
#1999=FACE_OUTER_BOUND ( 'NONE', #851, .T. ) ;
#2000=CARTESIAN_POINT ( 'NONE',  ( -1.187500000000000666, 4.275203145064813803, 6.771338133077573929 ) ) ;
#2009=AXIS2_PLACEMENT_3D ( 'NONE', #5325, #7232, #1613 ) ;
#2012=ORIENTED_EDGE ( 'NONE', *, *, #3139, .T. ) ;
#2017=( GEOMETRIC_REPRESENTATION_CONTEXT ( 3 ) GLOBAL_UNCERTAINTY_ASSIGNED_CONTEXT ( ( #5786 ) ) GLOBAL_UNIT_ASSIGNED_CONTEXT ( ( #7061, #291, #2181 ) ) REPRESENTATION_CONTEXT ( 'NONE', 'WORKASPACE' ) );
#2027=AXIS2_PLACEMENT_3D ( 'NONE', #4206, #2471, #6841 ) ;
#2032=ORIENTED_EDGE ( 'NONE', *, *, #8040, .F. ) ;
#2042=ADVANCED_FACE ( 'NONE', ( #6603 ), #5754, .T. ) ;
#2078=PLANE ( 'NONE',  #4912 ) ;
#2086=EDGE_CURVE ( 'NONE', #6380, #5098, #6612, .T. ) ;
#2096=CARTESIAN_POINT ( 'NONE',  ( 0.000000000000000000, 5.025000000000000355, 3.742515787401575533 ) ) ;
#2139=( BOUNDED_CURVE ( )  B_SPLINE_CURVE ( 3, ( #2763, #7203, #7930, #5248 ),
 .UNSPECIFIED., .F., .F. ) 
 B_SPLINE_CURVE_WITH_KNOTS ( ( 4, 4 ),
 ( 0.000000000000000000, 1.000000000000000000 ),
 .UNSPECIFIED. ) 
 CURVE ( )  GEOMETRIC_REPRESENTATION_ITEM ( )  RATIONAL_B_SPLINE_CURVE ( ( 1.000000000000000000, 0.8047378541243660477, 0.8047378541243660477, 1.000000000000000000 ) ) 
 REPRESENTATION_ITEM ( '' )  );
#2151=AXIS2_PLACEMENT_3D ( 'NONE', #4129, #7271, #7959 ) ;
#2157=FACE_OUTER_BOUND ( 'NONE', #5421, .T. ) ;
#2165=CARTESIAN_POINT ( 'NONE',  ( -2.375000000000000888, 2.762500000000000178, 6.956249999999999822 ) ) ;
#2166=AXIS2_PLACEMENT_3D ( 'NONE', #56, #2575, #1990 ) ;
#2169=CARTESIAN_POINT ( 'NONE',  ( 0.000000000000000000, 2.875000000000000888, 3.440250000000001140 ) ) ;
#2181=( NAMED_UNIT ( * ) SI_UNIT ( $, .STERADIAN. ) SOLID_ANGLE_UNIT ( ) );
#2210=CARTESIAN_POINT ( 'NONE',  ( -2.150000000000000799, 5.025000000000000355, 3.742515787401574645 ) ) ;
#2211=PLANE ( 'NONE',  #5579 ) ;
#2227=CARTESIAN_POINT ( 'NONE',  ( 3.121988307086614345, 2.389005866141732604, 4.968462007874016706 ) ) ;
#2233=CARTESIAN_POINT ( 'NONE',  ( -2.750000000000000444, 7.964000000000001300, 3.956249999995860911 ) ) ;
#2241=CARTESIAN_POINT ( 'NONE',  ( -3.121988307086614345, 5.510994133858267752, 4.968462007874016706 ) ) ;
#2243=CARTESIAN_POINT ( 'NONE',  ( -3.182000000000000828, 5.541000000000003922, 3.956250000000000266 ) ) ;
#2283=FACE_OUTER_BOUND ( 'NONE', #5377, .T. ) ;
#2295=CIRCLE ( 'NONE', #6094, 1.074999999999999289 ) ;
#2297=CLOSED_SHELL ( 'NONE', ( #7743, #6834, #5205, #4942, #102, #1595, #2042, #3429, #3498, #7738, #6763, #4867, #6159, #7423, #3671, #6696, #956, #8156, #5082 ) ) ;
#2309=EDGE_CURVE ( 'NONE', #533, #442, #945, .T. ) ;
#2337=CARTESIAN_POINT ( 'NONE',  ( -1.187500000000000222, 8.351123808764901568, 5.236250000000000959 ) ) ;
#2341=DIRECTION ( 'NONE',  ( 1.000000000000000000, -0.000000000000000000, 0.000000000000000000 ) ) ;
#2352=CARTESIAN_POINT ( 'NONE',  ( -1.388463899750249738E-31, 3.950000000000000178, 3.440250000000000696 ) ) ;
#2353=CARTESIAN_POINT ( 'NONE',  ( 0.000000000000000000, 2.523992677165354248, 5.972081456692916568 ) ) ;
#2371=CARTESIAN_POINT ( 'NONE',  ( 0.000000000000000000, 7.964000000000000412, 0.000000000000000000 ) ) ;
#2372=DIRECTION ( 'NONE',  ( -1.000000000000000000, 0.000000000000000000, -0.000000000000000000 ) ) ;
#2395=EDGE_CURVE ( 'NONE', #5001, #533, #7467, .T. ) ;
#2429=MECHANICAL_CONTEXT ( 'NONE', #6515, 'mechanical' ) ;
#2455=VECTOR ( 'NONE', #3064, 39.37007874015748143 ) ;
#2460=CARTESIAN_POINT ( 'NONE',  ( -1.187500000000000000, 5.969165905511811587, 6.858307716535433585 ) ) ;
#2461=CARTESIAN_POINT ( 'NONE',  ( 1.187500000000000444, 8.523567380006621619, 4.820336057633928029 ) ) ;
#2462=EDGE_LOOP ( 'NONE', ( #7552, #141, #787, #2032 ) ) ;
#2466=PLANE ( 'NONE',  #3574 ) ;
#2471=DIRECTION ( 'NONE',  ( 0.000000000000000000, 0.000000000000000000, -1.000000000000000000 ) ) ;
#2492=ORIENTED_EDGE ( 'NONE', *, *, #2309, .T. ) ;
#2494=CARTESIAN_POINT ( 'NONE',  ( 1.187500000000000444, 7.436775081392276832, 4.083473622006301262 ) ) ;
#2504=VERTEX_POINT ( 'NONE', #6875 ) ;
#2506=CARTESIAN_POINT ( 'NONE',  ( -1.187500000000000444, 4.186788071090408181, 6.858307717089314970 ) ) ;
#2509=ORIENTED_EDGE ( 'NONE', *, *, #2395, .T. ) ;
#2513=ORIENTED_EDGE ( 'NONE', *, *, #4877, .T. ) ;
#2515=VERTEX_POINT ( 'NONE', #6954 ) ;
#2527=AXIS2_PLACEMENT_3D ( 'NONE', #1081, #2962, #4846 ) ;
#2546=CARTESIAN_POINT ( 'NONE',  ( -1.187500000000000444, 4.734451501383331262, 5.775979225330971190 ) ) ;
#2547=VECTOR ( 'NONE', #1786, 39.37007874015748143 ) ;
#2575=DIRECTION ( 'NONE',  ( 1.000000000000000000, 0.000000000000000000, 0.000000000000000000 ) ) ;
#2582=DIRECTION ( 'NONE',  ( 0.000000000000000000, 0.000000000000000000, 1.000000000000000000 ) ) ;
#2584=CARTESIAN_POINT ( 'NONE',  ( -1.187500000000000666, 4.849020343544465206, 5.300059296325243530 ) ) ;
#2593=DIRECTION ( 'NONE',  ( 1.000000000000000000, 0.000000000000000000, 0.000000000000000000 ) ) ;
#2596=EDGE_LOOP ( 'NONE', ( #6204, #1487, #1238, #3458, #3246, #117, #4780, #5599 ) ) ;
#2606=DIRECTION ( 'NONE',  ( -1.000000000000000000, 0.000000000000000000, -0.000000000000000000 ) ) ;
#2607=CARTESIAN_POINT ( 'NONE',  ( 2.150000000000000799, 5.025000000000000355, 3.742515787401574645 ) ) ;
#2608=ORIENTED_EDGE ( 'NONE', *, *, #252, .F. ) ;
#2614=CARTESIAN_POINT ( 'NONE',  ( 0.000000000000000000, 5.539742775656026019, 3.998660959628785871 ) ) ;
#2623=CARTESIAN_POINT ( 'NONE',  ( -2.750000000000000444, 7.339000000000003077, 4.175863149606300340 ) ) ;
#2628=CARTESIAN_POINT ( 'NONE',  ( -4.936857409062767316E-17, 2.875000000000000444, 3.440250000000001140 ) ) ;
#2649=PLANE ( 'NONE',  #199 ) ;
#2657=CARTESIAN_POINT ( 'NONE',  ( 0.000000000000000000, 5.541000000000003034, 3.956250000000000266 ) ) ;
#2658=ORIENTED_EDGE ( 'NONE', *, *, #3526, .T. ) ;
#2665=CARTESIAN_POINT ( 'NONE',  ( -1.187499999999999778, 4.446597588353633057, 6.517308014370972735 ) ) ;
#2682=CARTESIAN_POINT ( 'NONE',  ( 1.074999999999999289, 3.950000000000000178, 3.440250000000000696 ) ) ;
#2702=EDGE_LOOP ( 'NONE', ( #4699, #6897, #1418, #4847, #2942 ) ) ;
#2707=CARTESIAN_POINT ( 'NONE',  ( -2.150000000000000799, 5.025000000000000355, 3.440250000000000696 ) ) ;
#2708=CARTESIAN_POINT ( 'NONE',  ( -2.750000000000000444, 8.574153543307087233, 4.323749999999999538 ) ) ;
#2713=CARTESIAN_POINT ( 'NONE',  ( 2.375000000000004441, 5.137500000000002842, 6.956249999999992717 ) ) ;
#2732=DIRECTION ( 'NONE',  ( -1.000000000000000000, 0.000000000000000000, 0.000000000000000000 ) ) ;
#2751=ORIENTED_EDGE ( 'NONE', *, *, #2309, .F. ) ;
#2754=ORIENTED_EDGE ( 'NONE', *, *, #8148, .T. ) ;
#2763=CARTESIAN_POINT ( 'NONE',  ( 0.000000000000000000, 2.359000000000000874, 3.956250000000000266 ) ) ;
#2764=CARTESIAN_POINT ( 'NONE',  ( 1.187500000000000444, 5.969165905511811587, 4.238473622047244760 ) ) ;
#2782=EDGE_CURVE ( 'NONE', #2992, #3502, #4370, .T. ) ;
#2787=CARTESIAN_POINT ( 'NONE',  ( -2.750000000000000444, 7.964000000000000412, 4.323750000000003091 ) ) ;
#2790=ORIENTED_EDGE ( 'NONE', *, *, #5629, .F. ) ;
#2799=CARTESIAN_POINT ( 'NONE',  ( 1.054418147088230118, 4.854198014699673713, 6.858307716535437137 ) ) ;
#2814=DIRECTION ( 'NONE',  ( -0.000000000000000000, -0.000000000000000000, 1.000000000000000000 ) ) ;
#2819=CARTESIAN_POINT ( 'NONE',  ( -3.182000000000000828, 5.541000000000003922, 3.956250000000000266 ) ) ;
#2831=( BOUNDED_SURFACE ( )  B_SPLINE_SURFACE ( 3, 3, ( 
 ( #723, #3217, #6379, #1298 ),
 ( #4525, #3822, #3788, #5596 ),
 ( #7039, #5722, #2607, #603 ),
 ( #1258, #1422, #4441, #5674 ) ),
 .UNSPECIFIED., .F., .F., .F. ) 
 B_SPLINE_SURFACE_WITH_KNOTS ( ( 4, 4 ),
 ( 4, 4 ),
 ( 0.000000000000000000, 1.000000000000000000 ),
 ( 0.000000000000000000, 1.000000000000000000 ),
 .UNSPECIFIED. ) 
 GEOMETRIC_REPRESENTATION_ITEM ( )  RATIONAL_B_SPLINE_SURFACE ( (
 ( 1.000000000000000000, 0.3333333333333330373, 0.3333333333333330373, 1.000000000000000000),
 ( 0.8047378541243660477, 0.2682459513747890156, 0.2682459513747890156, 0.8047378541243660477),
 ( 0.8047378541243660477, 0.2682459513747890156, 0.2682459513747890156, 0.8047378541243660477),
 ( 1.000000000000000000, 0.3333333333333330373, 0.3333333333333330373, 1.000000000000000000) ) ) 
 REPRESENTATION_ITEM ( '' )  SURFACE ( )  );
#2857=CARTESIAN_POINT ( 'NONE',  ( 0.000000000000000000, 5.376007322834645663, 5.972081456692916568 ) ) ;
#2866=ORIENTED_EDGE ( 'NONE', *, *, #239, .T. ) ;
#2879=LINE ( 'NONE', #7282, #3186 ) ;
#2887=DIRECTION ( 'NONE',  ( 0.000000000000000000, 0.000000000000000000, 1.000000000000000000 ) ) ;
#2898=EDGE_CURVE ( 'NONE', #5232, #6380, #3503, .T. ) ;
#2942=ORIENTED_EDGE ( 'NONE', *, *, #5367, .F. ) ;
#2946=LINE ( 'NONE', #1391, #3187 ) ;
#2953=SHAPE_DEFINITION_REPRESENTATION ( #7500, #4229 ) ;
#2962=DIRECTION ( 'NONE',  ( 1.000000000000000000, -0.000000000000000000, 2.606890220986081510E-17 ) ) ;
#2984=CARTESIAN_POINT ( 'NONE',  ( -1.187500000000000222, 4.987711023622046547, 4.083473622047245399 ) ) ;
#2992=VERTEX_POINT ( 'NONE', #802 ) ;
#2997=ORIENTED_EDGE ( 'NONE', *, *, #8040, .T. ) ;
#3053=DIRECTION ( 'NONE',  ( -0.000000000000000000, -0.000000000000000000, -1.000000000000000000 ) ) ;
#3064=DIRECTION ( 'NONE',  ( 1.000000000000000000, 0.000000000000000000, 0.000000000000000000 ) ) ;
#3083=DIMENSIONAL_EXPONENTS ( 1.000000000000000000, 0.000000000000000000, 0.000000000000000000, 0.000000000000000000, 0.000000000000000000, 0.000000000000000000, 0.000000000000000000 ) ;
#3098=( BOUNDED_CURVE ( )  B_SPLINE_CURVE ( 3, ( #3320, #2713, #4424, #3201 ),
 .UNSPECIFIED., .F., .T. ) 
 B_SPLINE_CURVE_WITH_KNOTS ( ( 4, 4 ),
 ( 0.000000000000000000, 0.09428240746600526079 ),
 .UNSPECIFIED. ) 
 CURVE ( )  GEOMETRIC_REPRESENTATION_ITEM ( )  RATIONAL_B_SPLINE_CURVE ( ( 1.000000000000000000, 0.3333333333333330373, 0.3333333333333330373, 1.000000000000000000 ) ) 
 REPRESENTATION_ITEM ( '' )  );
#3106=CARTESIAN_POINT ( 'NONE',  ( -2.375000000000003109, 5.137500000000000178, 6.956249999999992717 ) ) ;
#3139=EDGE_CURVE ( 'NONE', #3411, #5813, #165, .T. ) ;
#3141=CARTESIAN_POINT ( 'NONE',  ( 1.187500000000000444, 7.339000000000003965, 4.267772478794107371 ) ) ;
#3174=CARTESIAN_POINT ( 'NONE',  ( 1.187500000000000444, 7.964000000000000412, 5.236250000000000071 ) ) ;
#3176=VECTOR ( 'NONE', #3981, 39.37007874015748143 ) ;
#3177=VERTEX_POINT ( 'NONE', #4175 ) ;
#3186=VECTOR ( 'NONE', #1697, 39.37007874015748143 ) ;
#3187=VECTOR ( 'NONE', #4492, 39.37007874015748143 ) ;
#3191=ORIENTED_EDGE ( 'NONE', *, *, #3330, .T. ) ;
#3201=CARTESIAN_POINT ( 'NONE',  ( 0.000000000000000000, 2.762500000000000178, 6.956250000000000711 ) ) ;
#3205=ORIENTED_EDGE ( 'NONE', *, *, #1082, .T. ) ;
#3217=CARTESIAN_POINT ( 'NONE',  ( 3.182000000000000828, 2.359000000000000874, 3.956250000000000266 ) ) ;
#3218=DIRECTION ( 'NONE',  ( -0.000000000000000000, 1.000000000000000000, 0.000000000000000000 ) ) ;
#3220=ORIENTED_EDGE ( 'NONE', *, *, #4471, .F. ) ;
#3229=ORIENTED_EDGE ( 'NONE', *, *, #4877, .F. ) ;
#3232=FACE_OUTER_BOUND ( 'NONE', #4788, .T. ) ;
#3240=FACE_OUTER_BOUND ( 'NONE', #6935, .T. ) ;
#3244=ORIENTED_EDGE ( 'NONE', *, *, #1810, .F. ) ;
#3246=ORIENTED_EDGE ( 'NONE', *, *, #5184, .T. ) ;
#3270=CARTESIAN_POINT ( 'NONE',  ( -2.750000000000000444, 8.574153543168254288, 4.323749999249341336 ) ) ;
#3273=DIRECTION ( 'NONE',  ( -1.000000000000000000, 0.000000000000000000, 0.000000000000000000 ) ) ;
#3274=CARTESIAN_POINT ( 'NONE',  ( -1.187500000000000222, 4.913650942705939606, 4.937346008500399286 ) ) ;
#3313=CARTESIAN_POINT ( 'NONE',  ( -2.750000000000000444, 7.531471846334603981, 3.944609322583843891 ) ) ;
#3320=CARTESIAN_POINT ( 'NONE',  ( 0.000000000000000000, 5.137500000000000178, 6.956250000000000711 ) ) ;
#3330=EDGE_CURVE ( 'NONE', #2504, #5232, #6852, .T. ) ;
#3382=EDGE_CURVE ( 'NONE', #1162, #7981, #6145, .T. ) ;
#3393=ORIENTED_EDGE ( 'NONE', *, *, #4691, .F. ) ;
#3395=CARTESIAN_POINT ( 'NONE',  ( 0.000000000000000000, 5.510994133858271304, 4.968462007874015818 ) ) ;
#3411=VERTEX_POINT ( 'NONE', #3683 ) ;
#3429=ADVANCED_FACE ( 'NONE', ( #494 ), #4330, .T. ) ;
#3458=ORIENTED_EDGE ( 'NONE', *, *, #7872, .F. ) ;
#3461=FACE_OUTER_BOUND ( 'NONE', #5073, .T. ) ;
#3464=AXIS2_PLACEMENT_3D ( 'NONE', #8144, #4756, #1123 ) ;
#3467=ORIENTED_EDGE ( 'NONE', *, *, #441, .T. ) ;
#3485=CARTESIAN_POINT ( 'NONE',  ( 0.000000000000000000, 5.536672282146935409, 4.083473622047245399 ) ) ;
#3498=ADVANCED_FACE ( 'NONE', ( #8128 ), #2466, .T. ) ;
#3502=VERTEX_POINT ( 'NONE', #1685 ) ;
#3503=( BOUNDED_CURVE ( )  B_SPLINE_CURVE ( 3, ( #2657, #2614, #6600, #7250 ),
 .UNSPECIFIED., .F., .F. ) 
 B_SPLINE_CURVE_WITH_KNOTS ( ( 4, 4 ),
 ( 0.000000000000000000, 0.04204456198606273953 ),
 .UNSPECIFIED. ) 
 CURVE ( )  GEOMETRIC_REPRESENTATION_ITEM ( )  RATIONAL_B_SPLINE_CURVE ( ( 1.000000000000000000, 0.9998483700553054687, 0.9997031153252196045, 0.9995642358097424074 ) ) 
 REPRESENTATION_ITEM ( '' )  );
#3518=FACE_OUTER_BOUND ( 'NONE', #3980, .T. ) ;
#3526=EDGE_CURVE ( 'NONE', #805, #7672, #2946, .T. ) ;
#3535=DIRECTION ( 'NONE',  ( 1.000000000000000000, -1.016501579037865957E-15, 0.000000000000000000 ) ) ;
#3574=AXIS2_PLACEMENT_3D ( 'NONE', #4948, #7490, #1838 ) ;
#3577=CARTESIAN_POINT ( 'NONE',  ( 2.375000000000000888, 5.137500000000001066, 6.956249999999999822 ) ) ;
#3595=ORIENTED_EDGE ( 'NONE', *, *, #6291, .F. ) ;
#3596=CIRCLE ( 'NONE', #3464, 1.074999999999999289 ) ;
#3606=CARTESIAN_POINT ( 'NONE',  ( -1.187500000000000000, 8.523567361455139491, 4.820336051656679999 ) ) ;
#3623=CARTESIAN_POINT ( 'NONE',  ( 2.749999999999998668, 7.339000000000003077, 5.236250000000000071 ) ) ;
#3633=CARTESIAN_POINT ( 'NONE',  ( 1.187500000000000222, 4.232796286020916732, 6.817001420565361514 ) ) ;
#3648=CARTESIAN_POINT ( 'NONE',  ( -1.187499999717754884, 7.436775081331068016, 4.083473622121677415 ) ) ;
#3660=DIRECTION ( 'NONE',  ( 0.000000000000000000, 0.000000000000000000, -1.000000000000000000 ) ) ;
#3667=CARTESIAN_POINT ( 'NONE',  ( 1.187499999999999112, 4.849232312069990947, 5.299003540426529213 ) ) ;
#3671=ADVANCED_FACE ( 'NONE', ( #3461 ), #7049, .F. ) ;
#3683=CARTESIAN_POINT ( 'NONE',  ( -1.074999999999999289, 3.950000000000000178, -4.043750000000001066 ) ) ;
#3691=EDGE_LOOP ( 'NONE', ( #4923, #7452, #5215, #6753 ) ) ;
#3701=CARTESIAN_POINT ( 'NONE',  ( 2.750000000000000000, 7.521783346412262539, 3.956250000092213615 ) ) ;
#3702=CARTESIAN_POINT ( 'NONE',  ( 1.187500000000000000, 4.527538552213043133, 6.353289427497075259 ) ) ;
#3726=CARTESIAN_POINT ( 'NONE',  ( -1.054418134971605747, 4.854198021652829098, 6.858307716535429144 ) ) ;
#3736=CARTESIAN_POINT ( 'NONE',  ( 0.000000000000000000, 0.000000000000000000, 0.000000000000000000 ) ) ;
#3743=CARTESIAN_POINT ( 'NONE',  ( 1.187500000000000222, 4.620056610596821933, 6.126062285476682412 ) ) ;
#3748=ORIENTED_EDGE ( 'NONE', *, *, #2086, .F. ) ;
#3752=VECTOR ( 'NONE', #3218, 39.37007874015748143 ) ;
#3755=DIRECTION ( 'NONE',  ( -1.000000000000000000, 0.000000000000000000, 0.000000000000000000 ) ) ;
#3765=CARTESIAN_POINT ( 'NONE',  ( 0.000000000000000000, 5.145404907950669404, 6.923631455418962410 ) ) ;
#3767=CARTESIAN_POINT ( 'NONE',  ( -2.750000000000000444, 7.339000000000001300, 4.486250000000000959 ) ) ;
#3769=CARTESIAN_POINT ( 'NONE',  ( 3.182000000000000828, 5.541000000000003922, 3.956250000000000266 ) ) ;
#3772=ORIENTED_EDGE ( 'NONE', *, *, #1810, .T. ) ;
#3776=ORIENTED_EDGE ( 'NONE', *, *, #8030, .F. ) ;
#3781=CARTESIAN_POINT ( 'NONE',  ( 1.187500000000001110, 4.349209729547924397, 6.675164255166571081 ) ) ;
#3788=CARTESIAN_POINT ( 'NONE',  ( 2.577468385826771957, 5.238734212598424200, 3.956250000000000266 ) ) ;
#3800=CARTESIAN_POINT ( 'NONE',  ( -2.750000000000000444, 7.964000000000000412, 5.236250000000000071 ) ) ;
#3822=CARTESIAN_POINT ( 'NONE',  ( 2.577468385826771957, 2.661265787401575267, 3.956250000000000266 ) ) ;
#3839=CARTESIAN_POINT ( 'NONE',  ( -2.750000000000000444, 8.589000000000000412, 5.236250000000000071 ) ) ;
#3846=CIRCLE ( 'NONE', #7960, 2.619834133858267577 ) ;
#3880=CARTESIAN_POINT ( 'NONE',  ( -1.187500000000000000, 4.662394452531453126, 6.009229019005898564 ) ) ;
#3885=EDGE_LOOP ( 'NONE', ( #5907, #4272, #3467, #1657, #1514, #1048, #7501, #3913 ) ) ;
#3913=ORIENTED_EDGE ( 'NONE', *, *, #4152, .F. ) ;
#3915=CARTESIAN_POINT ( 'NONE',  ( -2.750000000000000444, 7.339000000000003077, 5.236250000000000071 ) ) ;
#3919=( BOUNDED_CURVE ( )  B_SPLINE_CURVE ( 2, ( #5760, #678, #3174, #7517, #6867, #3141, #2494 ),
 .UNSPECIFIED., .F., .T. ) 
 B_SPLINE_CURVE_WITH_KNOTS ( ( 3, 2, 2, 3 ),
 ( 0.000000000000000000, 0.01898937877529951676, 0.04622957262199210021, 0.05624330787783118901 ),
 .UNSPECIFIED. ) 
 CURVE ( )  GEOMETRIC_REPRESENTATION_ITEM ( )  RATIONAL_B_SPLINE_CURVE ( ( 0.8763122938253293803, 0.7958215604460294745, 1.000000000000000000, 0.7071067811865479058, 1.000000000000000000, 0.8923298722492541968, 0.8638207196608972405 ) ) 
 REPRESENTATION_ITEM ( '' )  );
#3947=CARTESIAN_POINT ( 'NONE',  ( 0.000000000000000000, 2.359000000000000874, 3.956250000000000266 ) ) ;
#3951=CARTESIAN_POINT ( 'NONE',  ( -2.750000000000000444, 7.521783346456695440, 3.956250000000000266 ) ) ;
#3979=CARTESIAN_POINT ( 'NONE',  ( 1.187500000000000444, 7.436775081392277720, 4.083473622006301262 ) ) ;
#3980=EDGE_LOOP ( 'NONE', ( #3205, #4065, #4777, #6270, #6034 ) ) ;
#3981=DIRECTION ( 'NONE',  ( -0.000000000000000000, 1.000000000000000000, 0.000000000000000000 ) ) ;
#4038=EDGE_CURVE ( 'NONE', #1162, #1366, #7730, .T. ) ;
#4065=ORIENTED_EDGE ( 'NONE', *, *, #3330, .F. ) ;
#4070=CARTESIAN_POINT ( 'NONE',  ( -2.852014645669292303, 2.523992677165354248, 5.972081456692913015 ) ) ;
#4077=EDGE_LOOP ( 'NONE', ( #1867, #6096 ) ) ;
#4129=CARTESIAN_POINT ( 'NONE',  ( -1.388463899750249738E-31, 3.950000000000000178, 3.440250000000000696 ) ) ;
#4139=CARTESIAN_POINT ( 'NONE',  ( 1.187500000722723215, 5.969165905511811587, 6.858307716535433585 ) ) ;
#4142=CARTESIAN_POINT ( 'NONE',  ( -2.750000000000000444, 7.964000000000000412, 4.323750000000003091 ) ) ;
#4152=EDGE_CURVE ( 'NONE', #5232, #5017, #6988, .T. ) ;
#4160=CARTESIAN_POINT ( 'NONE',  ( 1.187500002638678165, 4.186788052716939212, 6.858307716535433585 ) ) ;
#4175=CARTESIAN_POINT ( 'NONE',  ( -1.187500000000000444, 4.186788071090408181, 6.858307717089314970 ) ) ;
#4178=CARTESIAN_POINT ( 'NONE',  ( 0.000000000000000000, 2.762500000000000178, 6.956250000000000711 ) ) ;
#4203=DIRECTION ( 'NONE',  ( 0.000000000000000000, 1.000000000000000000, -0.000000000000000000 ) ) ;
#4206=CARTESIAN_POINT ( 'NONE',  ( -1.388463899750249738E-31, 3.950000000000000178, 3.440250000000000696 ) ) ;
#4214=CARTESIAN_POINT ( 'NONE',  ( 2.749999999999999556, 8.589000000000000412, 4.404023385826772774 ) ) ;
#4215=CARTESIAN_POINT ( 'NONE',  ( 2.852014645669292303, 2.523992677165354248, 5.972081456692913015 ) ) ;
#4229=SHAPE_REPRESENTATION ( 'bench vise3-', ( #7272 ), #2017 ) ;
#4241=ORIENTED_EDGE ( 'NONE', *, *, #3382, .F. ) ;
#4252=LINE ( 'NONE', #6879, #2455 ) ;
#4256=CARTESIAN_POINT ( 'NONE',  ( -1.187500000000000444, 4.186788071090408181, 6.858307717089314970 ) ) ;
#4272=ORIENTED_EDGE ( 'NONE', *, *, #2086, .T. ) ;
#4276=CARTESIAN_POINT ( 'NONE',  ( -1.388463899750249738E-31, 3.950000000000000178, -4.043750000000001066 ) ) ;
#4277=CARTESIAN_POINT ( 'NONE',  ( -2.750000000000000444, 7.964000000000000412, 3.956250000000000266 ) ) ;
#4280=CARTESIAN_POINT ( 'NONE',  ( 1.187499999999999778, 5.002317768095269734, 4.083473622031662309 ) ) ;
#4289=ORIENTED_EDGE ( 'NONE', *, *, #921, .F. ) ;
#4302=CARTESIAN_POINT ( 'NONE',  ( 0.000000000000000000, 5.510994133858271304, 4.968462007874015818 ) ) ;
#4316=CARTESIAN_POINT ( 'NONE',  ( 1.187499999999999778, 4.766431364955767691, 5.657758996208667845 ) ) ;
#4322=CARTESIAN_POINT ( 'NONE',  ( 0.4139007112234822094, 5.536672282146937185, 4.083473622047246288 ) ) ;
#4330=PLANE ( 'NONE',  #5003 ) ;
#4356=VECTOR ( 'NONE', #4203, 39.37007874015748143 ) ;
#4364=CARTESIAN_POINT ( 'NONE',  ( 0.000000000000000000, 5.137500000000000178, 6.956250000000000711 ) ) ;
#4370=LINE ( 'NONE', #6876, #5718 ) ;
#4383=CARTESIAN_POINT ( 'NONE',  ( 3.182000000000000828, 2.359000000000000874, 3.956250000000000266 ) ) ;
#4396=CARTESIAN_POINT ( 'NONE',  ( 1.187500000000000888, 4.383229855599106273, 6.623918406007527793 ) ) ;
#4420=CARTESIAN_POINT ( 'NONE',  ( -2.750000000000000888, 8.589000000000000412, 4.404023385826772774 ) ) ;
#4424=CARTESIAN_POINT ( 'NONE',  ( 2.375000000000004441, 2.762499999999999289, 6.956249999999992717 ) ) ;
#4441=CARTESIAN_POINT ( 'NONE',  ( 2.150000000000000799, 5.025000000000000355, 3.440250000000000696 ) ) ;
#4454=CARTESIAN_POINT ( 'NONE',  ( 0.000000000000000000, 5.137500000000000178, 6.956250000000000711 ) ) ;
#4456=LINE ( 'NONE', #6352, #5277 ) ;
#4465=LINE ( 'NONE', #7020, #4751 ) ;
#4471=EDGE_CURVE ( 'NONE', #1186, #1434, #3098, .T. ) ;
#4489=PRODUCT ( 'bench vise3-', 'bench vise3-', '', ( #2429 ) ) ;
#4492=DIRECTION ( 'NONE',  ( 1.000000000000000000, 0.000000000000000000, 0.000000000000000000 ) ) ;
#4499=CARTESIAN_POINT ( 'NONE',  ( -1.187499999999998002, 4.988117721439054186, 4.328788360466695018 ) ) ;
#4501=( BOUNDED_SURFACE ( )  B_SPLINE_SURFACE ( 3, 3, ( 
 ( #6479, #2243, #6569, #3947 ),
 ( #1023, #320, #5895, #7735 ),
 ( #6015, #2210, #7214, #5191 ),
 ( #5862, #2707, #937, #2169 ) ),
 .UNSPECIFIED., .F., .F., .T. ) 
 B_SPLINE_SURFACE_WITH_KNOTS ( ( 4, 4 ),
 ( 4, 4 ),
 ( 0.000000000000000000, 1.000000000000000000 ),
 ( 0.000000000000000000, 1.000000000000000000 ),
 .UNSPECIFIED. ) 
 GEOMETRIC_REPRESENTATION_ITEM ( )  RATIONAL_B_SPLINE_SURFACE ( (
 ( 1.000000000000000000, 0.3333333333333330373, 0.3333333333333330373, 1.000000000000000000),
 ( 0.8047378541243660477, 0.2682459513747890156, 0.2682459513747890156, 0.8047378541243660477),
 ( 0.8047378541243660477, 0.2682459513747890156, 0.2682459513747890156, 0.8047378541243660477),
 ( 1.000000000000000000, 0.3333333333333330373, 0.3333333333333330373, 1.000000000000000000) ) ) 
 REPRESENTATION_ITEM ( '' )  SURFACE ( )  );
#4525=CARTESIAN_POINT ( 'NONE',  ( 0.000000000000000000, 2.661265787401576155, 3.956250000000001155 ) ) ;
#4536=VECTOR ( 'NONE', #2341, 39.37007874015748143 ) ;
#4545=CARTESIAN_POINT ( 'NONE',  ( 2.750000000000000444, 8.589000000000000412, 5.236250000000000071 ) ) ;
#4570=LINE ( 'NONE', #351, #4773 ) ;
#4594=ORIENTED_EDGE ( 'NONE', *, *, #5224, .T. ) ;
#4601=LINE ( 'NONE', #1499, #3176 ) ;
#4602=EDGE_LOOP ( 'NONE', ( #3772, #4594, #2751, #8069 ) ) ;
#4607=DIRECTION ( 'NONE',  ( -0.000000000000000000, -0.000000000000000000, 1.000000000000000000 ) ) ;
#4629=( LENGTH_UNIT ( ) NAMED_UNIT ( * ) SI_UNIT ( $, .METRE. ) );
#4656=ORIENTED_EDGE ( 'NONE', *, *, #4691, .T. ) ;
#4685=CARTESIAN_POINT ( 'NONE',  ( -2.750000000000000444, 7.964000000000001300, 4.323750000000003091 ) ) ;
#4691=EDGE_CURVE ( 'NONE', #1965, #5413, #6580, .T. ) ;
#4699=ORIENTED_EDGE ( 'NONE', *, *, #6601, .T. ) ;
#4720=ORIENTED_EDGE ( 'NONE', *, *, #1133, .F. ) ;
#4732=CARTESIAN_POINT ( 'NONE',  ( 0.000000000000000000, 2.389005866141733492, 4.968462007874015818 ) ) ;
#4733=ORIENTED_EDGE ( 'NONE', *, *, #6291, .T. ) ;
#4739=ORIENTED_EDGE ( 'NONE', *, *, #5093, .T. ) ;
#4751=VECTOR ( 'NONE', #255, 39.37007874015748143 ) ;
#4756=DIRECTION ( 'NONE',  ( 0.000000000000000000, 0.000000000000000000, -1.000000000000000000 ) ) ;
#4757=CARTESIAN_POINT ( 'NONE',  ( 0.000000000000000000, 5.137500000000000178, 6.956250000000000711 ) ) ;
#4773=VECTOR ( 'NONE', #4607, 39.37007874015748143 ) ;
#4777=ORIENTED_EDGE ( 'NONE', *, *, #8044, .F. ) ;
#4780=ORIENTED_EDGE ( 'NONE', *, *, #6084, .T. ) ;
#4788=EDGE_LOOP ( 'NONE', ( #2997, #2513, #204, #2658 ) ) ;
#4799=EDGE_CURVE ( 'NONE', #1965, #805, #6710, .T. ) ;
#4824=FACE_OUTER_BOUND ( 'NONE', #3691, .T. ) ;
#4831=CARTESIAN_POINT ( 'NONE',  ( -1.187500000000000444, 7.339000000000001300, 4.486250000000000959 ) ) ;
#4846=DIRECTION ( 'NONE',  ( 5.213780441972162403E-17, 0.000000000000000000, -1.000000000000000000 ) ) ;
#4847=ORIENTED_EDGE ( 'NONE', *, *, #5828, .T. ) ;
#4861=DIRECTION ( 'NONE',  ( 0.000000000000000000, 1.000000000000000000, -0.000000000000000000 ) ) ;
#4867=ADVANCED_FACE ( 'NONE', ( #1999 ), #5032, .T. ) ;
#4874=CARTESIAN_POINT ( 'NONE',  ( 0.000000000000000000, 5.160877715062512472, 6.858307716807694909 ) ) ;
#4875=AXIS2_PLACEMENT_3D ( 'NONE', #1739, #5306, #6819 ) ;
#4877=EDGE_CURVE ( 'NONE', #5894, #1965, #4456, .T. ) ;
#4881=CARTESIAN_POINT ( 'NONE',  ( 2.749999999999999556, 7.521783346412262539, 3.956250000092213615 ) ) ;
#4903=PLANE ( 'NONE',  #587 ) ;
#4912=AXIS2_PLACEMENT_3D ( 'NONE', #7858, #2732, #2887 ) ;
#4914=( BOUNDED_CURVE ( )  B_SPLINE_CURVE ( 3, ( #5107, #7692, #5071, #1392 ),
 .UNSPECIFIED., .F., .F. ) 
 B_SPLINE_CURVE_WITH_KNOTS ( ( 4, 4 ),
 ( 8.186897041735312450E-13, 0.03375796088403870687 ),
 .UNSPECIFIED. ) 
 CURVE ( )  GEOMETRIC_REPRESENTATION_ITEM ( )  RATIONAL_B_SPLINE_CURVE ( ( 0.5716951606347142611, 0.6501402848013384528, 0.7927633098596811312, 0.9995642358097424074 ) ) 
 REPRESENTATION_ITEM ( '' )  );
#4923=ORIENTED_EDGE ( 'NONE', *, *, #7929, .T. ) ;
#4926=CARTESIAN_POINT ( 'NONE',  ( 2.749999999999999556, 8.589000000000000412, 4.486250000000000959 ) ) ;
#4932=DIRECTION ( 'NONE',  ( 1.000000000000000000, 0.000000000000000000, 0.000000000000000000 ) ) ;
#4939=CARTESIAN_POINT ( 'NONE',  ( 2.750000000000000444, 7.964000000000000412, 4.323750000000001315 ) ) ;
#4942=ADVANCED_FACE ( 'NONE', ( #3518 ), #4501, .T. ) ;
#4948=CARTESIAN_POINT ( 'NONE',  ( -1.201750000000000318, 5.151750000000000718, 6.956250000000000711 ) ) ;
#4958=ORIENTED_EDGE ( 'NONE', *, *, #6044, .T. ) ;
#5001=VERTEX_POINT ( 'NONE', #1473 ) ;
#5003=AXIS2_PLACEMENT_3D ( 'NONE', #2984, #5481, #8042 ) ;
#5017=VERTEX_POINT ( 'NONE', #6608 ) ;
#5032=PLANE ( 'NONE',  #980 ) ;
#5035=CARTESIAN_POINT ( 'NONE',  ( -1.187499999999999778, 4.553161336648244628, 6.294740251547498389 ) ) ;
#5071=CARTESIAN_POINT ( 'NONE',  ( -0.4139007109890988079, 5.536672282146934521, 4.083473622047245399 ) ) ;
#5073=EDGE_LOOP ( 'NONE', ( #4720, #6699, #3393, #3229 ) ) ;
#5076=FACE_BOUND ( 'NONE', #4602, .T. ) ;
#5082=ADVANCED_FACE ( 'N', ( #4824 ), #4903, .T. ) ;
#5093=EDGE_CURVE ( 'NONE', #7410, #3177, #8120, .T. ) ;
#5097=CARTESIAN_POINT ( 'NONE',  ( -2.375000000000003109, 2.762499999999999289, 6.956249999999992717 ) ) ;
#5098=VERTEX_POINT ( 'NONE', #7482 ) ;
#5107=CARTESIAN_POINT ( 'NONE',  ( -1.187499999443275334, 5.002317768720649482, 4.083473622047245399 ) ) ;
#5112=LINE ( 'NONE', #6054, #6367 ) ;
#5147=EDGE_LOOP ( 'NONE', ( #3191, #5619, #2866, #3776, #7210 ) ) ;
#5184=EDGE_CURVE ( 'NONE', #1434, #1186, #630, .T. ) ;
#5191=CARTESIAN_POINT ( 'NONE',  ( 0.000000000000000000, 2.875000000000000444, 3.742515787401575533 ) ) ;
#5205=ADVANCED_FACE ( 'NONE', ( #1864 ), #2831, .T. ) ;
#5215=ORIENTED_EDGE ( 'NONE', *, *, #7720, .F. ) ;
#5224=EDGE_CURVE ( 'NONE', #1117, #442, #3919, .T. ) ;
#5232=VERTEX_POINT ( 'NONE', #6911 ) ;
#5248=CARTESIAN_POINT ( 'NONE',  ( -4.936857409062767316E-17, 2.875000000000000444, 3.440250000000001140 ) ) ;
#5249=DIRECTION ( 'NONE',  ( -1.000000000000000000, 0.000000000000000000, -2.606890220986081510E-17 ) ) ;
#5258=CARTESIAN_POINT ( 'NONE',  ( 0.000000000000000000, 2.523992677165354248, 5.972081456692916568 ) ) ;
#5277=VECTOR ( 'NONE', #5773, 39.37007874015748143 ) ;
#5284=AXIS2_PLACEMENT_3D ( 'NONE', #2352, #3660, #3535 ) ;
#5297=DIRECTION ( 'NONE',  ( 1.000000000000000000, 0.000000000000000000, 0.000000000000000000 ) ) ;
#5304=CARTESIAN_POINT ( 'NONE',  ( -2.375000000000000888, 5.137500000000001066, 6.956249999999999822 ) ) ;
#5306=DIRECTION ( 'NONE',  ( -0.000000000000000000, 0.000000000000000000, 1.000000000000000000 ) ) ;
#5323=ORIENTED_EDGE ( 'NONE', *, *, #5184, .F. ) ;
#5325=CARTESIAN_POINT ( 'NONE',  ( 0.000000000000000000, 3.950000000000001954, 3.956250000000000266 ) ) ;
#5338=EDGE_LOOP ( 'NONE', ( #5323, #3220 ) ) ;
#5366=CARTESIAN_POINT ( 'NONE',  ( 0.000000000000000000, 2.389005866141733492, 4.968462007874016706 ) ) ;
#5367=EDGE_CURVE ( 'NONE', #5813, #7789, #6511, .T. ) ;
#5377=EDGE_LOOP ( 'NONE', ( #7761, #7072, #7342, #502 ) ) ;
#5383=CARTESIAN_POINT ( 'NONE',  ( 0.000000000000000000, 5.137500000000000178, 6.956250000000000711 ) ) ;
#5408=CARTESIAN_POINT ( 'NONE',  ( 2.749999999999998668, 8.589000000000000412, 5.236250000000000071 ) ) ;
#5413=VERTEX_POINT ( 'NONE', #4685 ) ;
#5421=EDGE_LOOP ( 'NONE', ( #2790, #2012, #6415, #81, #4958 ) ) ;
#5430=DIRECTION ( 'NONE',  ( -0.000000000000000000, -1.000000000000000000, 0.000000000000000000 ) ) ;
#5448=LINE ( 'NONE', #6035, #492 ) ;
#5449=B_SPLINE_CURVE_WITH_KNOTS ( 'NONE', 3,
 ( #4280, #7474, #1250, #6783, #1824, #3667, #7551, #4316, #6165, #1291, #6820, #3743, #1203, #6203, #3702, #5589, #8151, #1900, #4396, #3781, #1132, #1944, #6286, #3633, #6129, #7032 ),
 .UNSPECIFIED., .F., .F.,
 ( 4, 2, 2, 2, 2, 2, 2, 2, 2, 2, 2, 2, 4 ),
 ( 2.795095972151323432E-13, 0.01867100407285308614, 0.02800650610913988509, 0.03734200814542668750, 0.04667751018171348298, 0.05134526119985691195, 0.05601301221800034785, 0.06068076323614376988, 0.06534851425428719884, 0.06768238976335887169, 0.07001626527243054454, 0.07235014078150221739, 0.07468401629057389024 ),
 .UNSPECIFIED. ) ;
#5477=CARTESIAN_POINT ( 'NONE',  ( -1.187500000000000666, 7.339000000000003965, 4.267772478942485570 ) ) ;
#5479=EDGE_CURVE ( 'NONE', #7981, #1117, #7689, .T. ) ;
#5481=DIRECTION ( 'NONE',  ( 0.000000000000000000, 0.000000000000000000, -1.000000000000000000 ) ) ;
#5521=CARTESIAN_POINT ( 'NONE',  ( 3.121988307086614345, 5.510994133858267752, 4.968462007874016706 ) ) ;
#5572=CARTESIAN_POINT ( 'NONE',  ( 0.000000000000000000, 5.541000000000003034, 3.956250000000000266 ) ) ;
#5579=AXIS2_PLACEMENT_3D ( 'NONE', #1715, #484, #2372 ) ;
#5589=CARTESIAN_POINT ( 'NONE',  ( 1.187500000000000444, 4.474559027700158786, 6.463727320098461959 ) ) ;
#5596=CARTESIAN_POINT ( 'NONE',  ( 0.000000000000000000, 5.238734212598425088, 3.956250000000001155 ) ) ;
#5599=ORIENTED_EDGE ( 'NONE', *, *, #6152, .T. ) ;
#5618=DIRECTION ( 'NONE',  ( 1.000000000000000000, 0.000000000000000000, 0.000000000000000000 ) ) ;
#5619=ORIENTED_EDGE ( 'NONE', *, *, #4152, .T. ) ;
#5629=EDGE_CURVE ( 'NONE', #3411, #5792, #4465, .T. ) ;
#5630=CARTESIAN_POINT ( 'NONE',  ( 0.000000000000000000, 5.536672282146935409, 4.083473622047245399 ) ) ;
#5644=CARTESIAN_POINT ( 'NONE',  ( 2.750000000000000444, 7.339000000000003077, 4.175863149606300340 ) ) ;
#5671=VECTOR ( 'NONE', #6536, 39.37007874015748143 ) ;
#5674=CARTESIAN_POINT ( 'NONE',  ( 0.000000000000000000, 5.025000000000000355, 3.440250000000001140 ) ) ;
#5678=DIRECTION ( 'NONE',  ( 1.000000000000000000, 0.000000000000000000, 0.000000000000000000 ) ) ;
#5703=AXIS2_PLACEMENT_3D ( 'NONE', #5852, #2814, #5297 ) ;
#5718=VECTOR ( 'NONE', #6955, 39.37007874015748143 ) ;
#5722=CARTESIAN_POINT ( 'NONE',  ( 2.150000000000000799, 2.875000000000001332, 3.742515787401574645 ) ) ;
#5734=CARTESIAN_POINT ( 'NONE',  ( -2.750000000000000444, 8.589000000000000412, 4.486250000000000959 ) ) ;
#5742=FACE_OUTER_BOUND ( 'NONE', #3885, .T. ) ;
#5746=CARTESIAN_POINT ( 'NONE',  ( -1.187500000000000000, 5.969165905511811587, 4.238473622047244760 ) ) ;
#5754=( BOUNDED_SURFACE ( )  B_SPLINE_SURFACE ( 3, 3, ( 
 ( #5383, #5304, #2165, #1673 ),
 ( #2857, #5929, #4070, #5258 ),
 ( #3395, #2241, #5892, #4732 ),
 ( #316, #2819, #7253, #7990 ) ),
 .UNSPECIFIED., .F., .F., .F. ) 
 B_SPLINE_SURFACE_WITH_KNOTS ( ( 4, 4 ),
 ( 4, 4 ),
 ( 0.000000000000000000, 1.000000000000000000 ),
 ( 0.000000000000000000, 1.000000000000000000 ),
 .UNSPECIFIED. ) 
 GEOMETRIC_REPRESENTATION_ITEM ( )  RATIONAL_B_SPLINE_SURFACE ( (
 ( 1.000000000000000000, 0.3333333333333330373, 0.3333333333333330373, 1.000000000000000000),
 ( 0.9963935896217739341, 0.3321311965405909783, 0.3321311965405909783, 0.9963935896217739341),
 ( 0.9963935896217739341, 0.3321311965405909783, 0.3321311965405909783, 0.9963935896217739341),
 ( 1.000000000000000000, 0.3333333333333330373, 0.3333333333333330373, 1.000000000000000000) ) ) 
 REPRESENTATION_ITEM ( '' )  SURFACE ( )  );
#5760=CARTESIAN_POINT ( 'NONE',  ( 1.187500000000000444, 8.523567380006621619, 4.820336057633928917 ) ) ;
#5773=DIRECTION ( 'NONE',  ( -1.000000000000000000, -0.000000000000000000, -0.000000000000000000 ) ) ;
#5786=UNCERTAINTY_MEASURE_WITH_UNIT (LENGTH_MEASURE( 1.000000000000000082E-05 ), #7061, 'distance_accuracy_value', 'NONE');
#5792=VERTEX_POINT ( 'NONE', #909 ) ;
#5813=VERTEX_POINT ( 'NONE', #1647 ) ;
#5816=CARTESIAN_POINT ( 'NONE',  ( 2.750000000000000444, 7.531471846334603981, 3.944609322583843891 ) ) ;
#5828=EDGE_CURVE ( 'NONE', #2504, #7789, #6344, .T. ) ;
#5852=CARTESIAN_POINT ( 'NONE',  ( -1.388463899750249738E-31, 3.950000000000000178, -4.043750000000001066 ) ) ;
#5862=CARTESIAN_POINT ( 'NONE',  ( 0.000000000000000000, 5.025000000000000355, 3.440250000000001140 ) ) ;
#5868=CARTESIAN_POINT ( 'NONE',  ( 0.000000000000000000, 5.238734212598425977, 3.956250000000001155 ) ) ;
#5878=CARTESIAN_POINT ( 'NONE',  ( -1.187499999717754884, 7.436775081331068016, 4.083473622121677415 ) ) ;
#5892=CARTESIAN_POINT ( 'NONE',  ( -3.121988307086614345, 2.389005866141732604, 4.968462007874016706 ) ) ;
#5894=VERTEX_POINT ( 'NONE', #1689 ) ;
#5895=CARTESIAN_POINT ( 'NONE',  ( -2.577468385826771957, 2.661265787401575267, 3.956250000000000266 ) ) ;
#5907=ORIENTED_EDGE ( 'NONE', *, *, #2898, .T. ) ;
#5913=( BOUNDED_CURVE ( )  B_SPLINE_CURVE ( 2, ( #4881, #504, #8101, #3623, #6662, #5408, #4926, #4214, #7368 ),
 .UNSPECIFIED., .F., .T. ) 
 B_SPLINE_CURVE_WITH_KNOTS ( ( 3, 2, 2, 2, 3 ),
 ( 8.057829014928736820E-13, 0.01376350590615705097, 0.04131120849338899143, 0.06885891108062074106, 0.07294458655603817954 ),
 .UNSPECIFIED. ) 
 CURVE ( )  GEOMETRIC_REPRESENTATION_ITEM ( )  RATIONAL_B_SPLINE_CURVE ( ( 0.8535534732088591037, 0.8536633850130399548, 1.000000000000000000, 0.7071067811865479058, 1.000000000000000000, 0.7071067811865479058, 1.000000000000000000, 0.9565602018087399072, 0.9260057553135141450 ) ) 
 REPRESENTATION_ITEM ( '' )  );
#5929=CARTESIAN_POINT ( 'NONE',  ( -2.852014645669292303, 5.376007322834644775, 5.972081456692913015 ) ) ;
#5936=DIRECTION ( 'NONE',  ( -0.000000000000000000, -1.000000000000000000, -0.000000000000000000 ) ) ;
#5987=CARTESIAN_POINT ( 'NONE',  ( -1.187500000000000222, 7.339000000000003077, 5.236250000000000959 ) ) ;
#6012=ORIENTED_EDGE ( 'NONE', *, *, #6084, .F. ) ;
#6015=CARTESIAN_POINT ( 'NONE',  ( 0.000000000000000000, 5.024999999999999467, 3.742515787401575533 ) ) ;
#6024=APPLICATION_CONTEXT ( 'configuration controlled 3d designs of mechanical parts and assemblies' ) ;
#6034=ORIENTED_EDGE ( 'NONE', *, *, #239, .F. ) ;
#6035=CARTESIAN_POINT ( 'NONE',  ( -2.750000000000000444, 7.521783346456694552, 3.956250000000000266 ) ) ;
#6038=CARTESIAN_POINT ( 'NONE',  ( 1.187500002638678165, 4.186788052716939212, 6.858307716535433585 ) ) ;
#6044=EDGE_CURVE ( 'NONE', #7058, #5792, #1239, .T. ) ;
#6054=CARTESIAN_POINT ( 'NONE',  ( -1.187500000000000222, 5.969165905511811587, 6.858307716535433585 ) ) ;
#6062=AXIS2_PLACEMENT_3D ( 'NONE', #4276, #6811, #8054 ) ;
#6084=EDGE_CURVE ( 'NONE', #1366, #3177, #7026, .T. ) ;
#6094=AXIS2_PLACEMENT_3D ( 'NONE', #1265, #1869, #5678 ) ;
#6096=ORIENTED_EDGE ( 'NONE', *, *, #3139, .F. ) ;
#6129=CARTESIAN_POINT ( 'NONE',  ( 1.187500000000000222, 4.210703569520497958, 6.838410229878999047 ) ) ;
#6145=LINE ( 'NONE', #1723, #4356 ) ;
#6147=ORIENTED_EDGE ( 'NONE', *, *, #5479, .T. ) ;
#6152=EDGE_CURVE ( 'NONE', #3177, #2515, #7879, .T. ) ;
#6159=ADVANCED_FACE ( 'NONE', ( #3232, #5076 ), #1730, .T. ) ;
#6165=CARTESIAN_POINT ( 'NONE',  ( 1.187500000000000000, 4.734434094721707176, 5.776092429115636584 ) ) ;
#6203=CARTESIAN_POINT ( 'NONE',  ( 1.187499999999999778, 4.552120669721712254, 6.297178727289153954 ) ) ;
#6204=ORIENTED_EDGE ( 'NONE', *, *, #1931, .T. ) ;
#6225=VECTOR ( 'NONE', #7971, 39.37007874015748143 ) ;
#6237=DIRECTION ( 'NONE',  ( 0.000000000000000000, 0.000000000000000000, 1.000000000000000000 ) ) ;
#6270=ORIENTED_EDGE ( 'NONE', *, *, #6044, .F. ) ;
#6286=CARTESIAN_POINT ( 'NONE',  ( 1.187500000000000222, 4.274507914002040998, 6.772132732614807971 ) ) ;
#6291=EDGE_CURVE ( 'NONE', #442, #5098, #857, .T. ) ;
#6344=CIRCLE ( 'NONE', #2151, 1.074999999999999289 ) ;
#6352=CARTESIAN_POINT ( 'NONE',  ( 0.000000000000000000, 8.574153543307087233, 4.323750000000000426 ) ) ;
#6355=CARTESIAN_POINT ( 'NONE',  ( -1.187500000000000444, 4.384350929501749761, 6.623573783009716109 ) ) ;
#6367=VECTOR ( 'NONE', #401, 39.37007874015748143 ) ;
#6372=CARTESIAN_POINT ( 'NONE',  ( 0.000000000000000000, 5.137500000000000178, 6.956250000000000711 ) ) ;
#6379=CARTESIAN_POINT ( 'NONE',  ( 3.182000000000000828, 5.541000000000003922, 3.956250000000000266 ) ) ;
#6380=VERTEX_POINT ( 'NONE', #3485 ) ;
#6393=CARTESIAN_POINT ( 'NONE',  ( -1.187500000000000666, 4.766349921454176020, 5.658050103701500078 ) ) ;
#6415=ORIENTED_EDGE ( 'NONE', *, *, #5367, .T. ) ;
#6436=CARTESIAN_POINT ( 'NONE',  ( 2.750000000000000444, 7.339000000000003077, 5.236250000000000071 ) ) ;
#6459=AXIS2_PLACEMENT_3D ( 'NONE', #318, #1167, #4932 ) ;
#6479=CARTESIAN_POINT ( 'NONE',  ( 0.000000000000000000, 5.541000000000003034, 3.956250000000000266 ) ) ;
#6511=LINE ( 'NONE', #307, #7137 ) ;
#6515=APPLICATION_CONTEXT ( 'configuration controlled 3d designs of mechanical parts and assemblies' ) ;
#6536=DIRECTION ( 'NONE',  ( 0.000000000000000000, -1.000000000000000000, -0.000000000000000000 ) ) ;
#6569=CARTESIAN_POINT ( 'NONE',  ( -3.182000000000000828, 2.359000000000000874, 3.956250000000000266 ) ) ;
#6576=PRODUCT_DEFINITION_FORMATION_WITH_SPECIFIED_SOURCE ( 'ANY', '', #4489, .NOT_KNOWN. ) ;
#6580=LINE ( 'NONE', #2787, #5671 ) ;
#6600=CARTESIAN_POINT ( 'NONE',  ( 0.000000000000000000, 5.538300220770111082, 4.041069104531357148 ) ) ;
#6601=EDGE_CURVE ( 'NONE', #5813, #3411, #2295, .T. ) ;
#6603=FACE_OUTER_BOUND ( 'NONE', #2596, .T. ) ;
#6608=CARTESIAN_POINT ( 'NONE',  ( 0.000000000000000000, 2.359000000000000874, 3.956250000000000266 ) ) ;
#6612=( BOUNDED_CURVE ( )  B_SPLINE_CURVE ( 3, ( #5630, #4322, #1209, #1750 ),
 .UNSPECIFIED., .F., .F. ) 
 B_SPLINE_CURVE_WITH_KNOTS ( ( 4, 4 ),
 ( 0.000000000000000000, 0.03375796090494045942 ),
 .UNSPECIFIED. ) 
 CURVE ( )  GEOMETRIC_REPRESENTATION_ITEM ( )  RATIONAL_B_SPLINE_CURVE ( ( 0.9995642358097424074, 0.7927633097668024265, 0.6501402846732283747, 0.5716951605290202520 ) ) 
 REPRESENTATION_ITEM ( '' )  );
#6627=CARTESIAN_POINT ( 'NONE',  ( 0.5199956572608818162, 5.160877715126503951, 6.858307716535437137 ) ) ;
#6642=ORIENTED_EDGE ( 'NONE', *, *, #252, .T. ) ;
#6658=DIRECTION ( 'NONE',  ( 0.000000000000000000, 1.000000000000000000, 0.000000000000000000 ) ) ;
#6662=CARTESIAN_POINT ( 'NONE',  ( 2.749999999999999556, 7.964000000000000412, 5.236250000000000071 ) ) ;
#6664=CARTESIAN_POINT ( 'NONE',  ( -1.187500000000000000, 5.969165905511811587, 6.858307716535433585 ) ) ;
#6684=ORIENTED_EDGE ( 'NONE', *, *, #8148, .F. ) ;
#6696=ADVANCED_FACE ( 'NONE', ( #647 ), #7639, .T. ) ;
#6698=CYLINDRICAL_SURFACE ( 'NONE', #2527, 2.619834133858267577 ) ;
#6699=ORIENTED_EDGE ( 'NONE', *, *, #7929, .F. ) ;
#6701=DIRECTION ( 'NONE',  ( 1.986798540846736797E-16, 0.000000000000000000, 1.000000000000000000 ) ) ;
#6703=LINE ( 'NONE', #4277, #2547 ) ;
#6710=( BOUNDED_CURVE ( )  B_SPLINE_CURVE ( 2, ( #1309, #6882, #6961, #775, #3800, #1396, #3767, #1346, #654 ),
 .UNSPECIFIED., .F., .F. ) 
 B_SPLINE_CURVE_WITH_KNOTS ( ( 3, 2, 2, 2, 3 ),
 ( 1.913691129756523449E-11, 0.004098851392691885663, 0.03173539258822634379, 0.05937193378376098146, 0.07317982563254910033 ),
 .UNSPECIFIED. ) 
 CURVE ( )  GEOMETRIC_REPRESENTATION_ITEM ( )  RATIONAL_B_SPLINE_CURVE ( ( 0.9260057553135141450, 0.9565602018087399072, 1.000000000000000000, 0.7071067811865479058, 1.000000000000000000, 0.7071067811865479058, 1.000000000000000000, 0.8536633850130399548, 0.8535534732088591037 ) ) 
 REPRESENTATION_ITEM ( '' )  );
#6735=CARTESIAN_POINT ( 'NONE',  ( 0.000000000000000000, 5.376007322834645663, 5.972081456692916568 ) ) ;
#6744=FACE_OUTER_BOUND ( 'NONE', #2702, .T. ) ;
#6753=ORIENTED_EDGE ( 'NONE', *, *, #6772, .T. ) ;
#6763=ADVANCED_FACE ( 'NONE', ( #7564 ), #2078, .F. ) ;
#6764=CARTESIAN_POINT ( 'NONE',  ( 0.000000000000000000, 5.541000000000003034, 3.956250000000000266 ) ) ;
#6772=EDGE_CURVE ( 'NONE', #789, #5413, #4570, .T. ) ;
#6779=ORIENTED_EDGE ( 'NONE', *, *, #921, .T. ) ;
#6781=FACE_OUTER_BOUND ( 'NONE', #1813, .T. ) ;
#6783=CARTESIAN_POINT ( 'NONE',  ( 1.187500000000000444, 4.913748861513248301, 4.936700916451632004 ) ) ;
#6811=DIRECTION ( 'NONE',  ( -0.000000000000000000, -0.000000000000000000, 1.000000000000000000 ) ) ;
#6819=DIRECTION ( 'NONE',  ( 1.000000000000000000, 0.000000000000000000, 0.000000000000000000 ) ) ;
#6820=CARTESIAN_POINT ( 'NONE',  ( 1.187500000000000000, 4.660936287869686723, 6.010159138129464118 ) ) ;
#6834=ADVANCED_FACE ( 'NONE', ( #2157 ), #975, .T. ) ;
#6841=DIRECTION ( 'NONE',  ( 1.000000000000000000, 0.000000000000000000, 0.000000000000000000 ) ) ;
#6852=( BOUNDED_CURVE ( )  B_SPLINE_CURVE ( 3, ( #7744, #2096, #5868, #6764 ),
 .UNSPECIFIED., .F., .F. ) 
 B_SPLINE_CURVE_WITH_KNOTS ( ( 4, 4 ),
 ( 0.000000000000000000, 1.000000000000000000 ),
 .UNSPECIFIED. ) 
 CURVE ( )  GEOMETRIC_REPRESENTATION_ITEM ( )  RATIONAL_B_SPLINE_CURVE ( ( 1.000000000000000000, 0.8047378541243660477, 0.8047378541243660477, 1.000000000000000000 ) ) 
 REPRESENTATION_ITEM ( '' )  );
#6854=AXIS2_PLACEMENT_3D ( 'NONE', #4142, #6701, #1620 ) ;
#6867=CARTESIAN_POINT ( 'NONE',  ( 1.187500000000000444, 7.339000000000001300, 4.486250000000000959 ) ) ;
#6875=CARTESIAN_POINT ( 'NONE',  ( -6.890193713091687007E-11, 5.025000000000000355, 3.440250000000001140 ) ) ;
#6876=CARTESIAN_POINT ( 'NONE',  ( 2.750000000000000444, 7.964000000000000412, 5.246694173228347857 ) ) ;
#6879=CARTESIAN_POINT ( 'NONE',  ( 0.000000000000000000, 8.523567361303525658, 4.820336052022350160 ) ) ;
#6882=CARTESIAN_POINT ( 'NONE',  ( -2.750000000000000444, 8.589000000000000412, 4.404023385826772774 ) ) ;
#6883=CARTESIAN_POINT ( 'NONE',  ( -1.187500000000000888, 4.211027880314613725, 6.838140405204945260 ) ) ;
#6897=ORIENTED_EDGE ( 'NONE', *, *, #5629, .T. ) ;
#6904=ORIENTED_EDGE ( 'NONE', *, *, #4038, .F. ) ;
#6911=CARTESIAN_POINT ( 'NONE',  ( 0.000000000000000000, 5.541000000000003034, 3.956250000000000266 ) ) ;
#6926=CARTESIAN_POINT ( 'NONE',  ( 2.750000000000000444, 8.589000000000000412, 4.486250000000000959 ) ) ;
#6935=EDGE_LOOP ( 'NONE', ( #4656, #1198, #1287, #7702 ) ) ;
#6954=CARTESIAN_POINT ( 'NONE',  ( -1.187499999443275334, 5.002317768720649482, 4.083473622047245399 ) ) ;
#6955=DIRECTION ( 'NONE',  ( -0.000000000000000000, -0.000000000000000000, 1.000000000000000000 ) ) ;
#6961=CARTESIAN_POINT ( 'NONE',  ( -2.750000000000000444, 8.589000000000000412, 4.486250000000000959 ) ) ;
#6988=CIRCLE ( 'NONE', #2009, 1.591000000000001080 ) ;
#7011=CARTESIAN_POINT ( 'NONE',  ( 2.750000000000000888, 8.589000000000000412, 4.404023385826772774 ) ) ;
#7020=CARTESIAN_POINT ( 'NONE',  ( -1.074999999999999289, 3.950000000000000178, -4.043750000000001066 ) ) ;
#7026=( BOUNDED_CURVE ( )  B_SPLINE_CURVE ( 3, ( #1225, #1883, #3726, #4256 ),
 .UNSPECIFIED., .F., .F. ) 
 B_SPLINE_CURVE_WITH_KNOTS ( ( 4, 4 ),
 ( 2.728824016688292285E-13, 0.04207438243413257062 ),
 .UNSPECIFIED. ) 
 CURVE ( )  GEOMETRIC_REPRESENTATION_ITEM ( )  RATIONAL_B_SPLINE_CURVE ( ( 0.9996521287660724564, 0.6993327816080832093, 0.5343480788959518168, 0.5046980206296781679 ) ) 
 REPRESENTATION_ITEM ( '' )  );
#7031=LINE ( 'NONE', #7505, #6225 ) ;
#7032=CARTESIAN_POINT ( 'NONE',  ( 1.187500002638678165, 4.186788052716939212, 6.858307716535433585 ) ) ;
#7039=CARTESIAN_POINT ( 'NONE',  ( 0.000000000000000000, 2.875000000000000444, 3.742515787401575533 ) ) ;
#7049=PLANE ( 'NONE',  #6854 ) ;
#7055=CARTESIAN_POINT ( 'NONE',  ( -1.187500000000000666, 4.350832443807077787, 6.674940516136684820 ) ) ;
#7058=VERTEX_POINT ( 'NONE', #2628 ) ;
#7061=( CONVERSION_BASED_UNIT ( 'INCH', #864 ) LENGTH_UNIT ( ) NAMED_UNIT ( #3083 ) );
#7072=ORIENTED_EDGE ( 'NONE', *, *, #3526, .F. ) ;
#7091=CARTESIAN_POINT ( 'NONE',  ( 2.750000000000000444, 7.339000000000001300, 4.486250000000000959 ) ) ;
#7137=VECTOR ( 'NONE', #230, 39.37007874015748143 ) ;
#7152=CARTESIAN_POINT ( 'NONE',  ( 0.000000000000000000, 2.762500000000000178, 6.956250000000000711 ) ) ;
#7192=CARTESIAN_POINT ( 'NONE',  ( 0.000000000000000000, 2.359000000000000874, 3.956250000000000266 ) ) ;
#7201=CARTESIAN_POINT ( 'NONE',  ( -2.750000000000000444, 7.521783346469146814, 3.956249999992520916 ) ) ;
#7203=CARTESIAN_POINT ( 'NONE',  ( 0.000000000000000000, 2.661265787401576155, 3.956250000000001155 ) ) ;
#7210=ORIENTED_EDGE ( 'NONE', *, *, #5828, .F. ) ;
#7214=CARTESIAN_POINT ( 'NONE',  ( -2.150000000000000799, 2.875000000000001332, 3.742515787401574645 ) ) ;
#7232=DIRECTION ( 'NONE',  ( 0.000000000000000000, -0.000000000000000000, -1.000000000000000000 ) ) ;
#7239=EDGE_CURVE ( 'NONE', #7672, #2992, #4601, .T. ) ;
#7250=CARTESIAN_POINT ( 'NONE',  ( 0.000000000000000000, 5.536672282146935409, 4.083473622047245399 ) ) ;
#7253=CARTESIAN_POINT ( 'NONE',  ( -3.182000000000000828, 2.359000000000000874, 3.956250000000000266 ) ) ;
#7264=AXIS2_PLACEMENT_3D ( 'NONE', #2764, #5249, #510 ) ;
#7271=DIRECTION ( 'NONE',  ( 0.000000000000000000, 0.000000000000000000, -1.000000000000000000 ) ) ;
#7272=AXIS2_PLACEMENT_3D ( 'NONE', #3736, #6237, #5618 ) ;
#7282=CARTESIAN_POINT ( 'NONE',  ( -2.750000000000000444, 7.964000000000000412, 4.323750000000003091 ) ) ;
#7328=CARTESIAN_POINT ( 'NONE',  ( 0.000000000000000000, 5.160877715062512472, 6.858307716807694909 ) ) ;
#7342=ORIENTED_EDGE ( 'NONE', *, *, #1336, .T. ) ;
#7368=CARTESIAN_POINT ( 'NONE',  ( 2.750000000000000444, 8.574153540863029832, 4.323750000000001315 ) ) ;
#7410=VERTEX_POINT ( 'NONE', #6664 ) ;
#7417=CARTESIAN_POINT ( 'NONE',  ( 2.852014645669292303, 5.376007322834644775, 5.972081456692913015 ) ) ;
#7423=ADVANCED_FACE ( 'NONE', ( #467 ), #6698, .T. ) ;
#7452=ORIENTED_EDGE ( 'NONE', *, *, #2782, .F. ) ;
#7467=( BOUNDED_CURVE ( )  B_SPLINE_CURVE ( 2, ( #3606, #2337, #491, #5987, #4831, #5477, #3648 ),
 .UNSPECIFIED., .F., .F. ) 
 B_SPLINE_CURVE_WITH_KNOTS ( ( 3, 2, 2, 3 ),
 ( 9.875789629141308064E-12, 0.01898937877657074641, 0.04622957261936486151, 0.05624330786770232599 ),
 .UNSPECIFIED. ) 
 CURVE ( )  GEOMETRIC_REPRESENTATION_ITEM ( )  RATIONAL_B_SPLINE_CURVE ( ( 0.8763122937754233011, 0.7958215605093268419, 1.000000000000000000, 0.7071067811865479058, 1.000000000000000000, 0.8923298723145043354, 0.8638207196954514888 ) ) 
 REPRESENTATION_ITEM ( '' )  );
#7471=PLANE ( 'NONE',  #4875 ) ;
#7474=CARTESIAN_POINT ( 'NONE',  ( 1.187500000000000000, 4.988125073052579239, 4.328661356714555097 ) ) ;
#7482=CARTESIAN_POINT ( 'NONE',  ( 1.187499999999999778, 5.002317768095269734, 4.083473622031662309 ) ) ;
#7488=EDGE_CURVE ( 'NONE', #1366, #1186, #7626, .T. ) ;
#7490=DIRECTION ( 'NONE',  ( -0.000000000000000000, 0.000000000000000000, 1.000000000000000000 ) ) ;
#7492=CARTESIAN_POINT ( 'NONE',  ( 0.000000000000000000, 5.160877715062512472, 6.858307716807694909 ) ) ;
#7500=PRODUCT_DEFINITION_SHAPE ( 'NONE', 'NONE',  #1419 ) ;
#7501=ORIENTED_EDGE ( 'NONE', *, *, #7872, .T. ) ;
#7504=DIRECTION ( 'NONE',  ( -1.000000000000000000, 0.000000000000000000, -2.606890220986081510E-17 ) ) ;
#7505=CARTESIAN_POINT ( 'NONE',  ( -1.187499999435510212, 4.987711023622046547, 4.083473622047245399 ) ) ;
#7517=CARTESIAN_POINT ( 'NONE',  ( 1.187500000000000222, 7.339000000000003077, 5.236250000000000959 ) ) ;
#7518=CARTESIAN_POINT ( 'NONE',  ( 0.000000000000000000, 3.950000000000001954, 3.956250000000000266 ) ) ;
#7529=ORIENTED_EDGE ( 'NONE', *, *, #1931, .F. ) ;
#7551=CARTESIAN_POINT ( 'NONE',  ( 1.187500000000000000, 4.823830681599543979, 5.419287633353158107 ) ) ;
#7552=ORIENTED_EDGE ( 'NONE', *, *, #7239, .T. ) ;
#7564=FACE_OUTER_BOUND ( 'NONE', #981, .T. ) ;
#7572=CARTESIAN_POINT ( 'NONE',  ( -1.187500000000000222, 4.160767401574803515, 6.858307716535433585 ) ) ;
#7575=CARTESIAN_POINT ( 'NONE',  ( -1.187499999999999334, 4.622310746201133469, 6.124573350433617946 ) ) ;
#7578=CARTESIAN_POINT ( 'NONE',  ( 0.000000000000000000, 2.762500000000000178, 6.956250000000000711 ) ) ;
#7615=CARTESIAN_POINT ( 'NONE',  ( -2.750000000000000444, 7.339000000000001300, 4.486250000000000959 ) ) ;
#7626=( BOUNDED_CURVE ( )  B_SPLINE_CURVE ( 3, ( #7492, #565, #3765, #4454 ),
 .UNSPECIFIED., .F., .F. ) 
 B_SPLINE_CURVE_WITH_KNOTS ( ( 4, 4 ),
 ( 0.9667407784957844363, 1.000000000000000000 ),
 .UNSPECIFIED. ) 
 CURVE ( )  GEOMETRIC_REPRESENTATION_ITEM ( )  RATIONAL_B_SPLINE_CURVE ( ( 0.9996521287670052658, 0.9997640965207306163, 0.9998800535983954907, 1.000000000000000000 ) ) 
 REPRESENTATION_ITEM ( '' )  );
#7639=PLANE ( 'NONE',  #2166 ) ;
#7672=VERTEX_POINT ( 'NONE', #3701 ) ;
#7689=CIRCLE ( 'NONE', #7264, 2.619834133858267577 ) ;
#7692=CARTESIAN_POINT ( 'NONE',  ( -0.8527717963921712663, 5.380045629635501925, 4.083473622047245399 ) ) ;
#7700=CARTESIAN_POINT ( 'NONE',  ( -1.187500000000000222, 4.294835038531924276, 6.747773014656689661 ) ) ;
#7702=ORIENTED_EDGE ( 'NONE', *, *, #4799, .F. ) ;
#7720=EDGE_CURVE ( 'NONE', #789, #2992, #6703, .T. ) ;
#7730=( BOUNDED_CURVE ( )  B_SPLINE_CURVE ( 3, ( #6038, #2799, #6627, #7328 ),
 .UNSPECIFIED., .F., .F. ) 
 B_SPLINE_CURVE_WITH_KNOTS ( ( 4, 4 ),
 ( 4.504740859246951633E-12, 0.04207438291838416777 ),
 .UNSPECIFIED. ) 
 CURVE ( )  GEOMETRIC_REPRESENTATION_ITEM ( )  RATIONAL_B_SPLINE_CURVE ( ( 0.5046980198592107003, 0.5343480760378280792, 0.6993327790067819238, 0.9996521287660721233 ) ) 
 REPRESENTATION_ITEM ( '' )  );
#7735=CARTESIAN_POINT ( 'NONE',  ( 0.000000000000000000, 2.661265787401576155, 3.956250000000001155 ) ) ;
#7738=ADVANCED_FACE ( 'NONE', ( #6781 ), #7471, .T. ) ;
#7743=ADVANCED_FACE ( 'NONE', ( #6744 ), #8108, .T. ) ;
#7744=CARTESIAN_POINT ( 'NONE',  ( -6.890193713091687007E-11, 5.025000000000000355, 3.440250000000001140 ) ) ;
#7761=ORIENTED_EDGE ( 'NONE', *, *, #7239, .F. ) ;
#7789=VERTEX_POINT ( 'NONE', #2682 ) ;
#7829=CARTESIAN_POINT ( 'NONE',  ( -1.187500000000000222, 7.436775080912088498, 4.083473622047245399 ) ) ;
#7856=CIRCLE ( 'NONE', #621, 1.591000000000001080 ) ;
#7858=CARTESIAN_POINT ( 'NONE',  ( 1.187500000000000222, 4.160767401574803515, 6.858307716535433585 ) ) ;
#7864=MANIFOLD_SOLID_BREP ( 'Imported1', #2297 ) ;
#7872=EDGE_CURVE ( 'NONE', #1434, #5017, #8183, .T. ) ;
#7879=B_SPLINE_CURVE_WITH_KNOTS ( 'NONE', 3,
 ( #2506, #6883, #1278, #2000, #7700, #7055, #6355, #2665, #20, #68, #5035, #7575, #3880, #2546, #6393, #779, #2584, #1966, #3274, #1475, #4499, #1926 ),
 .UNSPECIFIED., .F., .F.,
 ( 4, 2, 2, 2, 2, 2, 2, 2, 2, 2, 4 ),
 ( 1.465475848683458973E-11, 0.002333053235454138254, 0.004666106456253518199, 0.009332212897852278088, 0.01399831933945103885, 0.01866442578104979960, 0.02799663866424725867, 0.03732885154744471773, 0.04666106443064217679, 0.05599327731383962892, 0.07465770308023454704 ),
 .UNSPECIFIED. ) ;
#7929=EDGE_CURVE ( 'NONE', #5413, #3502, #2879, .T. ) ;
#7930=CARTESIAN_POINT ( 'NONE',  ( 0.000000000000000000, 2.875000000000000888, 3.742515787401575533 ) ) ;
#7946=ORIENTED_EDGE ( 'NONE', *, *, #6152, .F. ) ;
#7959=DIRECTION ( 'NONE',  ( 1.000000000000000000, 1.524752368556799034E-15, 0.000000000000000000 ) ) ;
#7960=AXIS2_PLACEMENT_3D ( 'NONE', #5746, #7504, #1890 ) ;
#7966=DESIGN_CONTEXT ( 'detailed design', #6024, 'design' ) ;
#7971=DIRECTION ( 'NONE',  ( 0.000000000000000000, 1.000000000000000000, 0.000000000000000000 ) ) ;
#7981=VERTEX_POINT ( 'NONE', #4139 ) ;
#7990=CARTESIAN_POINT ( 'NONE',  ( 0.000000000000000000, 2.359000000000000874, 3.956250000000000266 ) ) ;
#8010=EDGE_LOOP ( 'NONE', ( #4733, #3748, #7529, #6642, #2492 ) ) ;
#8030=EDGE_CURVE ( 'NONE', #7789, #7058, #3596, .T. ) ;
#8040=EDGE_CURVE ( 'NONE', #7672, #5894, #5913, .T. ) ;
#8042=DIRECTION ( 'NONE',  ( -1.000000000000000000, 0.000000000000000000, -0.000000000000000000 ) ) ;
#8044=EDGE_CURVE ( 'NONE', #5792, #2504, #717, .T. ) ;
#8054=DIRECTION ( 'NONE',  ( 1.000000000000000000, 0.000000000000000000, 0.000000000000000000 ) ) ;
#8069=ORIENTED_EDGE ( 'NONE', *, *, #2395, .F. ) ;
#8101=CARTESIAN_POINT ( 'NONE',  ( 2.749999999999999556, 7.339000000000001300, 4.486250000000000959 ) ) ;
#8108=CYLINDRICAL_SURFACE ( 'NONE', #6459, 1.074999999999999289 ) ;
#8120=LINE ( 'NONE', #2460, #1374 ) ;
#8128=FACE_OUTER_BOUND ( 'NONE', #5338, .T. ) ;
#8144=CARTESIAN_POINT ( 'NONE',  ( -1.388463899750249738E-31, 3.950000000000000178, 3.440250000000000696 ) ) ;
#8148=EDGE_CURVE ( 'NONE', #7410, #5001, #3846, .T. ) ;
#8151=CARTESIAN_POINT ( 'NONE',  ( 1.187500000000000000, 4.446184378179288466, 6.518065150780170569 ) ) ;
#8156=ADVANCED_FACE ( 'NONE', ( #3240 ), #76, .F. ) ;
#8183=( BOUNDED_CURVE ( )  B_SPLINE_CURVE ( 3, ( #7152, #875, #5366, #7192 ),
 .UNSPECIFIED., .F., .F. ) 
 B_SPLINE_CURVE_WITH_KNOTS ( ( 4, 4 ),
 ( 0.000000000000000000, 1.000000000000000000 ),
 .UNSPECIFIED. ) 
 CURVE ( )  GEOMETRIC_REPRESENTATION_ITEM ( )  RATIONAL_B_SPLINE_CURVE ( ( 1.000000000000000000, 0.9963935896217739341, 0.9963935896217739341, 1.000000000000000000 ) ) 
 REPRESENTATION_ITEM ( '' )  );
#8227=COLOUR_RGB('Light Gray', 0.08235294, 0.09019608, 0.10196078);
#8228=FILL_AREA_STYLE_COLOUR('',#8227);
#8229=FILL_AREA_STYLE('',(#8228));
#8230=SURFACE_STYLE_FILL_AREA(#8229);
#8231=SURFACE_SIDE_STYLE('',(#8230));
#8232=SURFACE_STYLE_USAGE(.BOTH.,#8231);
#8233=PRESENTATION_STYLE_ASSIGNMENT((#8232));
#8247=STYLED_ITEM('',(#8233),#7864);
#8248=MECHANICAL_DESIGN_GEOMETRIC_PRESENTATION_REPRESENTATION('',(#8247),#2017);
ENDSEC;
END-ISO-10303-21;
